ISO-10303-21;
HEADER;
FILE_DESCRIPTION (('STEP AP214'),
    '1' );
FILE_NAME ('instrument roller bearing_iso_ISO 1224 - 171015 - R,24,SI,NC,24.step',
    '2026-10-08T08:02:49',
    ( '' ),
    ( '' ),
    'SwSTEP 2.0',
    'SolidWorks 2026',
    '' );
FILE_SCHEMA (( 'AUTOMOTIVE_DESIGN' ));
ENDSEC;

DATA;
#43=CARTESIAN_POINT ( 'NONE',  ( -1.200000000000006617, 0.000000000000000000, 0.000000000000000000 ) ) ;
#66=EDGE_LOOP ( 'NONE', ( #17110, #3171, #49258, #1993 ) ) ;
#104=AXIS2_PLACEMENT_3D ( 'NONE', #50216, #16097, #21404 ) ;
#159=CARTESIAN_POINT ( 'NONE',  ( 1.500000000000001332, 9.123618653647810742E-16, 7.400000000000022560 ) ) ;
#207=ORIENTED_EDGE ( 'NONE', *, *, #11032, .T. ) ;
#219=VERTEX_POINT ( 'NONE', #37023 ) ;
#276=ADVANCED_FACE ( 'NONE', ( #10344 ), #14742, .T. ) ;
#277=EDGE_LOOP ( 'NONE', ( #3307, #822 ) ) ;
#291=DIRECTION ( 'NONE',  ( 0.000000000000000000, 0.000000000000000000, -1.000000000000000000 ) ) ;
#381=CARTESIAN_POINT ( 'NONE',  ( -1.399999999999998579, 9.184850993605175555E-16, 7.500000000000022204 ) ) ;
#403=DIRECTION ( 'NONE',  ( 0.000000000000000000, 0.000000000000000000, 1.000000000000000000 ) ) ;
#472=VERTEX_POINT ( 'NONE', #13670 ) ;
#518=CIRCLE ( 'NONE', #13553, 5.612499999999999822 ) ;
#626=DIRECTION ( 'NONE',  ( 1.000000000000000000, 0.000000000000000000, 0.000000000000000000 ) ) ;
#666=DIRECTION ( 'NONE',  ( 1.000000000000000000, 0.000000000000000000, 0.000000000000000000 ) ) ;
#699=LINE ( 'NONE', #38957, #41739 ) ;
#775=CIRCLE ( 'NONE', #19798, 5.612499999999999822 ) ;
#804=DIRECTION ( 'NONE',  ( -1.000000000000000000, 0.000000000000000000, -0.000000000000000000 ) ) ;
#806=TOROIDAL_SURFACE ( 'NONE', #38851, 7.400000000000022560, 0.09999999999999961697 ) ;
#813=DIRECTION ( 'NONE',  ( 0.000000000000000000, 0.000000000000000000, -1.000000000000000000 ) ) ;
#822=ORIENTED_EDGE ( 'NONE', *, *, #2768, .T. ) ;
#875=ORIENTED_EDGE ( 'NONE', *, *, #14039, .T. ) ;
#964=CIRCLE ( 'NONE', #42008, 7.400000000000021672 ) ;
#994=ORIENTED_EDGE ( 'NONE', *, *, #2396, .T. ) ;
#1033=ADVANCED_FACE ( 'NONE', ( #49241 ), #29825, .F. ) ;
#1132=CARTESIAN_POINT ( 'NONE',  ( -1.200000000000006617, 6.873330160214519262E-16, 5.612499999999999822 ) ) ;
#1145=ORIENTED_EDGE ( 'NONE', *, *, #12252, .T. ) ;
#1164=DIRECTION ( 'NONE',  ( 0.000000000000000000, 0.000000000000000000, -1.000000000000000000 ) ) ;
#1175=FACE_BOUND ( 'NONE', #17045, .T. ) ;
#1177=VERTEX_POINT ( 'NONE', #2229 ) ;
#1182=ORIENTED_EDGE ( 'NONE', *, *, #29135, .F. ) ;
#1204=( LENGTH_UNIT ( ) NAMED_UNIT ( * ) SI_UNIT ( .MILLI., .METRE. ) );
#1267=AXIS2_PLACEMENT_3D ( 'NONE', #56128, #32657, #60824 ) ;
#1314=CIRCLE ( 'NONE', #36387, 0.02570000000000176310 ) ;
#1399=FACE_BOUND ( 'NONE', #17286, .T. ) ;
#1424=LINE ( 'NONE', #15869, #46163 ) ;
#1444=AXIS2_PLACEMENT_3D ( 'NONE', #21886, #41315, #26887 ) ;
#1563=CARTESIAN_POINT ( 'NONE',  ( -1.399999999999998579, 0.000000000000000000, 0.000000000000000000 ) ) ;
#1583=TOROIDAL_SURFACE ( 'NONE', #25619, 7.400000000000021672, 0.1000000000000001582 ) ;
#1688=DIRECTION ( 'NONE',  ( 0.000000000000000000, 0.000000000000000000, -1.000000000000000000 ) ) ;
#1725=VERTEX_POINT ( 'NONE', #38529 ) ;
#1759=AXIS2_PLACEMENT_3D ( 'NONE', #7101, #2724, #17772 ) ;
#1790=FACE_OUTER_BOUND ( 'NONE', #6223, .T. ) ;
#1795=DIRECTION ( 'NONE',  ( 1.000000000000000000, 0.000000000000000000, 0.000000000000000000 ) ) ;
#1835=CARTESIAN_POINT ( 'NONE',  ( -1.500000000000001332, 0.000000000000000000, 0.000000000000000000 ) ) ;
#1873=CARTESIAN_POINT ( 'NONE',  ( -90.00000000000000000, 0.000000000000000000, 0.000000000000000000 ) ) ;
#1993=ORIENTED_EDGE ( 'NONE', *, *, #31136, .F. ) ;
#2031=DIRECTION ( 'NONE',  ( 1.000000000000000000, -0.000000000000000000, -0.000000000000000000 ) ) ;
#2066=VERTEX_POINT ( 'NONE', #14033 ) ;
#2073=CARTESIAN_POINT ( 'NONE',  ( -1.500000000000001332, 0.000000000000000000, 0.000000000000000000 ) ) ;
#2168=EDGE_CURVE ( 'NONE', #59631, #48937, #1424, .T. ) ;
#2203=CIRCLE ( 'NONE', #18248, 6.866799999999992465 ) ;
#2229=CARTESIAN_POINT ( 'NONE',  ( -1.500000000000001332, 0.000000000000000000, -6.728125000000022560 ) ) ;
#2339=AXIS2_PLACEMENT_3D ( 'NONE', #28791, #14100, #43223 ) ;
#2373=CYLINDRICAL_SURFACE ( 'NONE', #28066, 7.500000000000022204 ) ;
#2396=EDGE_CURVE ( 'NONE', #31646, #45810, #15179, .T. ) ;
#2519=EDGE_CURVE ( 'NONE', #14527, #30513, #42153, .T. ) ;
#2676=ORIENTED_EDGE ( 'NONE', *, *, #53167, .T. ) ;
#2724=DIRECTION ( 'NONE',  ( 1.000000000000000000, 0.000000000000000000, 0.000000000000000000 ) ) ;
#2735=DIRECTION ( 'NONE',  ( 0.000000000000000000, 0.000000000000000000, -1.000000000000000000 ) ) ;
#2749=EDGE_CURVE ( 'NONE', #46714, #25119, #18114, .T. ) ;
#2768=EDGE_CURVE ( 'NONE', #61018, #60897, #54119, .T. ) ;
#2815=SURFACE_STYLE_USAGE ( .BOTH. , #26634 ) ;
#2867=ORIENTED_EDGE ( 'NONE', *, *, #42320, .T. ) ;
#3084=DIRECTION ( 'NONE',  ( 0.000000000000000000, 0.000000000000000000, -1.000000000000000000 ) ) ;
#3129=CARTESIAN_POINT ( 'NONE',  ( -1.114299999999999846, 0.000000000000000000, 0.000000000000000000 ) ) ;
#3171=ORIENTED_EDGE ( 'NONE', *, *, #41295, .T. ) ;
#3220=ORIENTED_EDGE ( 'NONE', *, *, #48384, .T. ) ;
#3250=EDGE_CURVE ( 'NONE', #45810, #22775, #10917, .T. ) ;
#3307=ORIENTED_EDGE ( 'NONE', *, *, #22758, .T. ) ;
#3320=DIRECTION ( 'NONE',  ( 1.000000000000000000, 0.000000000000000000, 0.000000000000000000 ) ) ;
#3345=FACE_OUTER_BOUND ( 'NONE', #44724, .T. ) ;
#3428=DIRECTION ( 'NONE',  ( 0.000000000000000000, 0.000000000000000000, -1.000000000000000000 ) ) ;
#3524=EDGE_LOOP ( 'NONE', ( #31887, #42957, #22308, #14831 ) ) ;
#3600=DIRECTION ( 'NONE',  ( 1.000000000000000000, 0.000000000000000000, 0.000000000000000000 ) ) ;
#3618=CARTESIAN_POINT ( 'NONE',  ( -1.200000000000006617, 0.000000000000000000, 0.000000000000000000 ) ) ;
#3638=AXIS2_PLACEMENT_3D ( 'NONE', #31623, #16605, #16291 ) ;
#3718=ADVANCED_FACE ( 'NONE', ( #25110 ), #46924, .T. ) ;
#3759=CARTESIAN_POINT ( 'NONE',  ( 0.000000000000000000, 0.000000000000000000, 0.000000000000000000 ) ) ;
#3834=VERTEX_POINT ( 'NONE', #21970 ) ;
#3855=AXIS2_PLACEMENT_3D ( 'NONE', #28346, #13342, #51520 ) ;
#3933=ORIENTED_EDGE ( 'NONE', *, *, #32790, .F. ) ;
#3942=ORIENTED_EDGE ( 'NONE', *, *, #6996, .T. ) ;
#4037=FILL_AREA_STYLE_COLOUR ( '', #22710 ) ;
#4056=CARTESIAN_POINT ( 'NONE',  ( 1.499999999999999556, 5.100000000000000533, 0.000000000000000000 ) ) ;
#4110=FACE_OUTER_BOUND ( 'NONE', #56973, .T. ) ;
#4121=AXIS2_PLACEMENT_3D ( 'NONE', #29998, #53777, #5853 ) ;
#4140=UNCERTAINTY_MEASURE_WITH_UNIT (LENGTH_MEASURE( 1.000000000000000082E-05 ), #18478, 'distance_accuracy_value', 'NONE');
#4153=ORIENTED_EDGE ( 'NONE', *, *, #23919, .F. ) ;
#4191=FACE_BOUND ( 'NONE', #45738, .T. ) ;
#4256=VECTOR ( 'NONE', #58844, 1000.000000000000000 ) ;
#4261=ADVANCED_FACE ( 'NONE', ( #45952 ), #2373, .T. ) ;
#4262=CARTESIAN_POINT ( 'NONE',  ( -90.00000000000000000, 0.000000000000000000, 0.000000000000000000 ) ) ;
#4277=AXIS2_PLACEMENT_3D ( 'NONE', #39956, #6676, #39027 ) ;
#4435=AXIS2_PLACEMENT_3D ( 'NONE', #39525, #5637, #24783 ) ;
#4454=DIRECTION ( 'NONE',  ( 1.000000000000000000, 0.000000000000000000, 0.000000000000000000 ) ) ;
#4532=DIRECTION ( 'NONE',  ( 0.000000000000000000, 0.000000000000000000, -1.000000000000000000 ) ) ;
#4769=TOROIDAL_SURFACE ( 'NONE', #12829, 5.633200000000004870, 0.02570000000000154800 ) ;
#4787=VECTOR ( 'NONE', #626, 1000.000000000000000 ) ;
#4808=CARTESIAN_POINT ( 'NONE',  ( -1.139999999999998570, 0.000000000000000000, -6.866799999999992465 ) ) ;
#4882=CYLINDRICAL_SURFACE ( 'NONE', #58784, 5.612499999999999822 ) ;
#4949=CARTESIAN_POINT ( 'NONE',  ( -1.400000000000000355, 0.000000000000000000, 0.000000000000000000 ) ) ;
#4986=DIRECTION ( 'NONE',  ( -1.000000000000000000, 0.000000000000000000, -0.000000000000000000 ) ) ;
#5003=ORIENTED_EDGE ( 'NONE', *, *, #41797, .F. ) ;
#5065=ADVANCED_FACE ( 'NONE', ( #29430, #28196 ), #5298, .T. ) ;
#5100=ORIENTED_EDGE ( 'NONE', *, *, #57322, .F. ) ;
#5110=AXIS2_PLACEMENT_3D ( 'NONE', #43, #666, #19806 ) ;
#5197=LINE ( 'NONE', #47525, #49347 ) ;
#5202=VECTOR ( 'NONE', #50152, 1000.000000000000000 ) ;
#5217=DIRECTION ( 'NONE',  ( 0.000000000000000000, 0.000000000000000000, 1.000000000000000000 ) ) ;
#5298=PLANE ( 'NONE',  #21950 ) ;
#5340=CARTESIAN_POINT ( 'NONE',  ( -1.400000000000000355, 0.000000000000000000, 0.000000000000000000 ) ) ;
#5483=DIRECTION ( 'NONE',  ( -0.000000000000000000, 0.000000000000000000, 1.000000000000000000 ) ) ;
#5495=ORIENTED_EDGE ( 'NONE', *, *, #39561, .T. ) ;
#5533=ORIENTED_EDGE ( 'NONE', *, *, #30909, .T. ) ;
#5630=DIRECTION ( 'NONE',  ( 1.000000000000000000, 0.000000000000000000, 0.000000000000000000 ) ) ;
#5637=DIRECTION ( 'NONE',  ( 1.000000000000000000, 0.000000000000000000, 0.000000000000000000 ) ) ;
#5647=DIRECTION ( 'NONE',  ( 0.000000000000000000, 0.000000000000000000, -1.000000000000000000 ) ) ;
#5678=DIRECTION ( 'NONE',  ( 0.000000000000000000, 0.000000000000000000, -1.000000000000000000 ) ) ;
#5717=CARTESIAN_POINT ( 'NONE',  ( -1.200000000000006617, 6.873330160214519262E-16, 5.612499999999999822 ) ) ;
#5755=CIRCLE ( 'NONE', #22782, 5.612499999999999822 ) ;
#5812=CARTESIAN_POINT ( 'NONE',  ( 1.199999999999992628, 6.873330160214519262E-16, 5.612499999999999822 ) ) ;
#5842=ORIENTED_EDGE ( 'NONE', *, *, #39412, .T. ) ;
#5853=DIRECTION ( 'NONE',  ( 0.000000000000000000, 0.000000000000000000, -1.000000000000000000 ) ) ;
#5916=DIRECTION ( 'NONE',  ( 0.000000000000000000, 0.000000000000000000, -1.000000000000000000 ) ) ;
#5996=FACE_BOUND ( 'NONE', #46835, .T. ) ;
#6000=AXIS2_PLACEMENT_3D ( 'NONE', #12570, #22266, #56373 ) ;
#6193=EDGE_CURVE ( 'NONE', #46370, #10577, #53802, .T. ) ;
#6223=EDGE_LOOP ( 'NONE', ( #51618, #46364 ) ) ;
#6234=CARTESIAN_POINT ( 'NONE',  ( 1.199999999999992628, 8.239576745513314221E-16, 6.728125000000023448 ) ) ;
#6299=ORIENTED_EDGE ( 'NONE', *, *, #28873, .T. ) ;
#6347=DIRECTION ( 'NONE',  ( 1.000000000000000000, -0.000000000000000000, -0.000000000000000000 ) ) ;
#6384=EDGE_CURVE ( 'NONE', #21245, #34877, #49845, .T. ) ;
#6396=CARTESIAN_POINT ( 'NONE',  ( -90.00000000000000000, 6.873330160214519262E-16, 5.612499999999999822 ) ) ;
#6543=CARTESIAN_POINT ( 'NONE',  ( 1.399999999999999467, 0.000000000000000000, 0.000000000000000000 ) ) ;
#6569=DIRECTION ( 'NONE',  ( 1.000000000000000000, -0.000000000000000000, -0.000000000000000000 ) ) ;
#6659=( GEOMETRIC_REPRESENTATION_CONTEXT ( 3 ) GLOBAL_UNCERTAINTY_ASSIGNED_CONTEXT ( ( #4140 ) ) GLOBAL_UNIT_ASSIGNED_CONTEXT ( ( #18478, #51047, #17252 ) ) REPRESENTATION_CONTEXT ( 'NONE', 'WORKASPACE' ) );
#6676=DIRECTION ( 'NONE',  ( 1.000000000000000000, 0.000000000000000000, 0.000000000000000000 ) ) ;
#6772=VECTOR ( 'NONE', #38678, 1000.000000000000114 ) ;
#6850=DIRECTION ( 'NONE',  ( 1.000000000000000000, 0.000000000000000000, 0.000000000000000000 ) ) ;
#6902=LINE ( 'NONE', #22579, #49253 ) ;
#6960=DIRECTION ( 'NONE',  ( 0.000000000000000000, 0.000000000000000000, -1.000000000000000000 ) ) ;
#6992=AXIS2_PLACEMENT_3D ( 'NONE', #54101, #59743, #11222 ) ;
#6996=EDGE_CURVE ( 'NONE', #219, #61755, #53252, .T. ) ;
#7100=EDGE_CURVE ( 'NONE', #61755, #46275, #19545, .T. ) ;
#7101=CARTESIAN_POINT ( 'NONE',  ( 1.399999999999999467, 0.000000000000000000, 0.000000000000000000 ) ) ;
#7242=ORIENTED_EDGE ( 'NONE', *, *, #25967, .F. ) ;
#7258=CARTESIAN_POINT ( 'NONE',  ( -1.139999999999999680, 6.866799999999992465, 0.000000000000000000 ) ) ;
#7271=CYLINDRICAL_SURFACE ( 'NONE', #38250, 5.000000000000000888 ) ;
#7494=EDGE_CURVE ( 'NONE', #14527, #19512, #20565, .T. ) ;
#7506=DIRECTION ( 'NONE',  ( 0.000000000000000000, 1.224646799147353207E-16, 1.000000000000000000 ) ) ;
#7519=CARTESIAN_POINT ( 'NONE',  ( 1.140000000000009006, 0.000000000000000000, 0.000000000000000000 ) ) ;
#7524=DIRECTION ( 'NONE',  ( 1.000000000000000000, 0.000000000000000000, 0.000000000000000000 ) ) ;
#7590=AXIS2_PLACEMENT_3D ( 'NONE', #27190, #17183, #27489 ) ;
#7596=DIRECTION ( 'NONE',  ( 0.000000000000000000, 1.000000000000000000, -1.224646799147353207E-16 ) ) ;
#7620=TOROIDAL_SURFACE ( 'NONE', #50641, 5.633200000000004870, 0.02570000000000154800 ) ;
#7685=ORIENTED_EDGE ( 'NONE', *, *, #56701, .F. ) ;
#7687=CYLINDRICAL_SURFACE ( 'NONE', #19196, 6.887500000000022382 ) ;
#7743=CIRCLE ( 'NONE', #43832, 6.728125000000022560 ) ;
#7788=CARTESIAN_POINT ( 'NONE',  ( -1.129531546211723025, 0.000000000000000000, 0.000000000000000000 ) ) ;
#7883=FACE_OUTER_BOUND ( 'NONE', #52234, .T. ) ;
#7998=DIRECTION ( 'NONE',  ( 0.000000000000000000, 1.000000000000000000, -1.224646799147353207E-16 ) ) ;
#8064=DIRECTION ( 'NONE',  ( 0.000000000000000000, 0.000000000000000000, -1.000000000000000000 ) ) ;
#8125=DIRECTION ( 'NONE',  ( 0.000000000000000000, 0.000000000000000000, -1.000000000000000000 ) ) ;
#8175=VERTEX_POINT ( 'NONE', #381 ) ;
#8330=VECTOR ( 'NONE', #21946, 1000.000000000000000 ) ;
#8334=CARTESIAN_POINT ( 'NONE',  ( -1.200000000000000622, 6.887500000000022382, 0.000000000000000000 ) ) ;
#8473=VERTEX_POINT ( 'NONE', #24139 ) ;
#8512=EDGE_CURVE ( 'NONE', #3834, #23453, #47048, .T. ) ;
#8515=CARTESIAN_POINT ( 'NONE',  ( -90.00000000000000000, 0.000000000000000000, 0.000000000000000000 ) ) ;
#8520=ADVANCED_FACE ( 'NONE', ( #14151 ), #45489, .T. ) ;
#8563=VERTEX_POINT ( 'NONE', #6234 ) ;
#8613=DIRECTION ( 'NONE',  ( 1.000000000000000000, 0.000000000000000000, 0.000000000000000000 ) ) ;
#8671=ORIENTED_EDGE ( 'NONE', *, *, #32346, .F. ) ;
#8677=CARTESIAN_POINT ( 'NONE',  ( -1.129531546211723025, 6.886005254585696675E-16, 5.612499999999999822 ) ) ;
#8718=ORIENTED_EDGE ( 'NONE', *, *, #28282, .F. ) ;
#8766=DIRECTION ( 'NONE',  ( 1.000000000000000000, 0.000000000000000000, 0.000000000000000000 ) ) ;
#8777=FACE_OUTER_BOUND ( 'NONE', #56708, .T. ) ;
#8783=ORIENTED_EDGE ( 'NONE', *, *, #50750, .T. ) ;
#8853=DIRECTION ( 'NONE',  ( 0.000000000000000000, 0.000000000000000000, -1.000000000000000000 ) ) ;
#8903=AXIS2_PLACEMENT_3D ( 'NONE', #61895, #29030, #43150 ) ;
#9132=CYLINDRICAL_SURFACE ( 'NONE', #51717, 6.887500000000022382 ) ;
#9182=ADVANCED_FACE ( 'NONE', ( #15451 ), #24848, .F. ) ;
#9458=DIRECTION ( 'NONE',  ( 1.000000000000000000, 0.000000000000000000, 0.000000000000000000 ) ) ;
#9500=EDGE_CURVE ( 'NONE', #2066, #3834, #13506, .T. ) ;
#9640=CARTESIAN_POINT ( 'NONE',  ( -1.400000000000000799, 0.000000000000000000, 0.000000000000000000 ) ) ;
#9645=AXIS2_PLACEMENT_3D ( 'NONE', #3618, #13063, #22753 ) ;
#9820=EDGE_CURVE ( 'NONE', #34877, #31646, #17524, .T. ) ;
#9929=DIRECTION ( 'NONE',  ( 1.000000000000000000, 0.000000000000000000, 0.000000000000000000 ) ) ;
#10153=CARTESIAN_POINT ( 'NONE',  ( 1.140000000000004343, 5.633200000000004870, 0.000000000000000000 ) ) ;
#10187=FACE_OUTER_BOUND ( 'NONE', #26628, .T. ) ;
#10281=AXIS2_PLACEMENT_3D ( 'NONE', #36082, #46097, #40791 ) ;
#10344=FACE_OUTER_BOUND ( 'NONE', #55218, .T. ) ;
#10365=CARTESIAN_POINT ( 'NONE',  ( 1.199999999999992628, 0.000000000000000000, 0.000000000000000000 ) ) ;
#10373=AXIS2_PLACEMENT_3D ( 'NONE', #14401, #14709, #52901 ) ;
#10375=EDGE_LOOP ( 'NONE', ( #55963, #31004, #46719, #50409 ) ) ;
#10388=DIRECTION ( 'NONE',  ( 0.000000000000000000, 0.000000000000000000, -1.000000000000000000 ) ) ;
#10413=CIRCLE ( 'NONE', #51389, 6.887500000000022382 ) ;
#10427=CIRCLE ( 'NONE', #36470, 0.1000000000000002554 ) ;
#10448=CARTESIAN_POINT ( 'NONE',  ( -1.139999999999998570, 8.422079734756228398E-16, 6.866799999999992465 ) ) ;
#10565=EDGE_CURVE ( 'NONE', #25757, #37959, #26848, .T. ) ;
#10577=VERTEX_POINT ( 'NONE', #59840 ) ;
#10622=CARTESIAN_POINT ( 'NONE',  ( -1.139999999999999902, 6.898680348956876061E-16, 5.633200000000004870 ) ) ;
#10633=ADVANCED_FACE ( 'NONE', ( #46084 ), #4769, .T. ) ;
#10646=AXIS2_PLACEMENT_3D ( 'NONE', #43757, #804, #5483 ) ;
#10702=AXIS2_PLACEMENT_3D ( 'NONE', #4056, #28192, #52296 ) ;
#10780=VECTOR ( 'NONE', #33497, 1000.000000000000000 ) ;
#10817=ORIENTED_EDGE ( 'NONE', *, *, #25967, .T. ) ;
#10851=CARTESIAN_POINT ( 'NONE',  ( 1.399999999999999467, 6.245698675651501825E-16, 5.100000000000000533 ) ) ;
#10859=MANIFOLD_SOLID_BREP ( 'InnerRace', #36069 ) ;
#10887=VECTOR ( 'NONE', #31731, 1000.000000000000114 ) ;
#10890=ORIENTED_EDGE ( 'NONE', *, *, #41797, .T. ) ;
#10917=CIRCLE ( 'NONE', #3855, 7.500000000000022204 ) ;
#10952=FACE_OUTER_BOUND ( 'NONE', #24730, .T. ) ;
#10995=CARTESIAN_POINT ( 'NONE',  ( -90.00000000000000000, 0.000000000000000000, -5.612499999999999822 ) ) ;
#11032=EDGE_CURVE ( 'NONE', #59631, #22147, #27748, .T. ) ;
#11056=FACE_OUTER_BOUND ( 'NONE', #24528, .T. ) ;
#11083=CARTESIAN_POINT ( 'NONE',  ( -1.200000000000006617, 0.000000000000000000, 0.000000000000000000 ) ) ;
#11222=DIRECTION ( 'NONE',  ( 0.000000000000000000, 0.000000000000000000, 1.000000000000000000 ) ) ;
#11241=SURFACE_STYLE_FILL_AREA ( #40387 ) ;
#11281=DIRECTION ( 'NONE',  ( 1.000000000000000000, 0.000000000000000000, 0.000000000000000000 ) ) ;
#11291=DIRECTION ( 'NONE',  ( 0.000000000000000000, 0.000000000000000000, -1.000000000000000000 ) ) ;
#11328=DIRECTION ( 'NONE',  ( 1.000000000000000000, 0.000000000000000000, 0.000000000000000000 ) ) ;
#11381=ADVANCED_FACE ( 'NONE', ( #18647 ), #56833, .T. ) ;
#11497=ORIENTED_EDGE ( 'NONE', *, *, #10565, .F. ) ;
#11550=AXIS2_PLACEMENT_3D ( 'NONE', #51617, #51004, #13748 ) ;
#11576=VERTEX_POINT ( 'NONE', #17639 ) ;
#11597=CARTESIAN_POINT ( 'NONE',  ( 1.199999999999992628, 0.000000000000000000, 0.000000000000000000 ) ) ;
#11606=ORIENTED_EDGE ( 'NONE', *, *, #13492, .T. ) ;
#11630=CARTESIAN_POINT ( 'NONE',  ( 1.129531546211701931, 0.000000000000000000, 0.000000000000000000 ) ) ;
#11643=AXIS2_PLACEMENT_3D ( 'NONE', #11630, #6569, #35445 ) ;
#11723=STYLED_ITEM ( 'NONE', ( #45770 ), #59429 ) ;
#11771=AXIS2_PLACEMENT_3D ( 'NONE', #11597, #11281, #25372 ) ;
#11859=DIRECTION ( 'NONE',  ( 0.000000000000000000, 0.000000000000000000, -1.000000000000000000 ) ) ;
#11911=EDGE_CURVE ( 'NONE', #60182, #36274, #775, .T. ) ;
#11951=EDGE_LOOP ( 'NONE', ( #20283, #19938, #17863, #24935 ) ) ;
#12017=CIRCLE ( 'NONE', #20016, 5.612499999999999822 ) ;
#12065=DIRECTION ( 'NONE',  ( 1.000000000000000000, -0.000000000000000000, -0.000000000000000000 ) ) ;
#12252=EDGE_CURVE ( 'NONE', #48937, #20219, #5755, .T. ) ;
#12262=EDGE_CURVE ( 'NONE', #23932, #1177, #7743, .T. ) ;
#12387=CARTESIAN_POINT ( 'NONE',  ( -1.200000000000006617, 8.239576745513313235E-16, 6.728125000000022560 ) ) ;
#12404=DIRECTION ( 'NONE',  ( 1.000000000000000000, 0.000000000000000000, 0.000000000000000000 ) ) ;
#12465=CARTESIAN_POINT ( 'NONE',  ( -1.400000000000000799, 0.000000000000000000, -7.400000000000021672 ) ) ;
#12570=CARTESIAN_POINT ( 'NONE',  ( -1.500000000000001332, 0.000000000000000000, 0.000000000000000000 ) ) ;
#12573=CARTESIAN_POINT ( 'NONE',  ( -1.129531546211723025, 0.000000000000000000, -5.612499999999999822 ) ) ;
#12639=CIRCLE ( 'NONE', #29597, 6.728125000000022560 ) ;
#12660=CARTESIAN_POINT ( 'NONE',  ( 1.399999999999999023, 0.000000000000000000, -7.400000000000022560 ) ) ;
#12816=ORIENTED_EDGE ( 'NONE', *, *, #21515, .T. ) ;
#12820=AXIS2_PLACEMENT_3D ( 'NONE', #46925, #55353, #8064 ) ;
#12829=AXIS2_PLACEMENT_3D ( 'NONE', #3129, #46381, #23178 ) ;
#13035=ADVANCED_FACE ( 'NONE', ( #47022, #42023 ), #32922, .T. ) ;
#13052=ORIENTED_EDGE ( 'NONE', *, *, #12262, .F. ) ;
#13063=DIRECTION ( 'NONE',  ( 1.000000000000000000, 0.000000000000000000, 0.000000000000000000 ) ) ;
#13171=DIRECTION ( 'NONE',  ( 0.000000000000000000, 1.000000000000000000, -1.224646799147353207E-16 ) ) ;
#13250=EDGE_CURVE ( 'NONE', #19512, #14527, #45776, .T. ) ;
#13261=CYLINDRICAL_SURFACE ( 'NONE', #21338, 5.612499999999999822 ) ;
#13262=EDGE_LOOP ( 'NONE', ( #42285, #21849, #48684, #61867 ) ) ;
#13342=DIRECTION ( 'NONE',  ( 1.000000000000000000, 0.000000000000000000, 0.000000000000000000 ) ) ;
#13433=DIRECTION ( 'NONE',  ( 0.000000000000000000, 0.000000000000000000, -1.000000000000000000 ) ) ;
#13447=EDGE_CURVE ( 'NONE', #47186, #43343, #12639, .T. ) ;
#13458=LINE ( 'NONE', #23459, #10780 ) ;
#13461=ORIENTED_EDGE ( 'NONE', *, *, #53167, .F. ) ;
#13492=EDGE_CURVE ( 'NONE', #40053, #11576, #28615, .T. ) ;
#13506=CIRCLE ( 'NONE', #58501, 5.000000000000000000 ) ;
#13510=CIRCLE ( 'NONE', #37581, 5.100000000000000533 ) ;
#13535=ORIENTED_EDGE ( 'NONE', *, *, #9500, .F. ) ;
#13553=AXIS2_PLACEMENT_3D ( 'NONE', #49161, #30986, #36021 ) ;
#13633=ORIENTED_EDGE ( 'NONE', *, *, #13250, .F. ) ;
#13654=DIRECTION ( 'NONE',  ( 0.000000000000000000, 0.000000000000000000, -1.000000000000000000 ) ) ;
#13670=CARTESIAN_POINT ( 'NONE',  ( 1.199999999999992628, 0.000000000000000000, -6.887500000000022382 ) ) ;
#13733=DIRECTION ( 'NONE',  ( 0.000000000000000000, 0.000000000000000000, -1.000000000000000000 ) ) ;
#13748=DIRECTION ( 'NONE',  ( 0.000000000000000000, 1.224646799147353947E-16, 1.000000000000000000 ) ) ;
#13770=AXIS2_PLACEMENT_3D ( 'NONE', #33066, #28340, #47456 ) ;
#13822=DIRECTION ( 'NONE',  ( 1.000000000000000000, 0.000000000000000000, 0.000000000000000000 ) ) ;
#13998=ORIENTED_EDGE ( 'NONE', *, *, #9820, .F. ) ;
#14033=CARTESIAN_POINT ( 'NONE',  ( -1.399999999999998579, 0.000000000000000000, -5.000000000000000000 ) ) ;
#14039=EDGE_CURVE ( 'NONE', #30513, #32528, #51591, .T. ) ;
#14049=EDGE_CURVE ( 'NONE', #11576, #37959, #19653, .T. ) ;
#14100=DIRECTION ( 'NONE',  ( 1.000000000000000000, -0.000000000000000000, -0.000000000000000000 ) ) ;
#14151=FACE_OUTER_BOUND ( 'NONE', #54077, .T. ) ;
#14227=DIRECTION ( 'NONE',  ( 0.000000000000000000, 0.000000000000000000, -1.000000000000000000 ) ) ;
#14235=ORIENTED_EDGE ( 'NONE', *, *, #29933, .F. ) ;
#14280=AXIS2_PLACEMENT_3D ( 'NONE', #33220, #60767, #56379 ) ;
#14292=ORIENTED_EDGE ( 'NONE', *, *, #13447, .T. ) ;
#14362=EDGE_CURVE ( 'NONE', #40053, #25757, #27685, .T. ) ;
#14401=CARTESIAN_POINT ( 'NONE',  ( 1.399999999999998579, 0.000000000000000000, 0.000000000000000000 ) ) ;
#14491=CARTESIAN_POINT ( 'NONE',  ( 1.500000000000001332, 0.000000000000000000, 0.000000000000000000 ) ) ;
#14527=VERTEX_POINT ( 'NONE', #12573 ) ;
#14528=EDGE_LOOP ( 'NONE', ( #31221, #40275, #53163, #47948 ) ) ;
#14652=DIRECTION ( 'NONE',  ( 0.000000000000000000, 0.000000000000000000, -1.000000000000000000 ) ) ;
#14677=AXIS2_PLACEMENT_3D ( 'NONE', #3759, #61387, #13822 ) ;
#14709=DIRECTION ( 'NONE',  ( 1.000000000000000000, 0.000000000000000000, 0.000000000000000000 ) ) ;
#14742=CYLINDRICAL_SURFACE ( 'NONE', #48074, 5.612499999999999822 ) ;
#14759=TOROIDAL_SURFACE ( 'NONE', #22747, 6.866799999999992465, 0.02570000000000859444 ) ;
#14831=ORIENTED_EDGE ( 'NONE', *, *, #21515, .F. ) ;
#14852=ORIENTED_EDGE ( 'NONE', *, *, #50476, .T. ) ;
#14869=ORIENTED_EDGE ( 'NONE', *, *, #2396, .F. ) ;
#14993=FACE_OUTER_BOUND ( 'NONE', #47263, .T. ) ;
#15001=PLANE ( 'NONE',  #59412 ) ;
#15168=LINE ( 'NONE', #5717, #6772 ) ;
#15171=DIRECTION ( 'NONE',  ( -0.000000000000000000, 0.000000000000000000, -1.000000000000000000 ) ) ;
#15179=LINE ( 'NONE', #39000, #50126 ) ;
#15229=VERTEX_POINT ( 'NONE', #57842 ) ;
#15251=DIRECTION ( 'NONE',  ( -0.8831157194574164038, 0.000000000000000000, 0.4691552259617384202 ) ) ;
#15367=ADVANCED_FACE ( 'NONE', ( #55299 ), #7687, .F. ) ;
#15389=CIRCLE ( 'NONE', #2339, 5.633200000000004870 ) ;
#15410=DIRECTION ( 'NONE',  ( -1.000000000000000000, 0.000000000000000000, 0.000000000000000000 ) ) ;
#15423=ORIENTED_EDGE ( 'NONE', *, *, #45629, .T. ) ;
#15451=FACE_OUTER_BOUND ( 'NONE', #51970, .T. ) ;
#15593=DIRECTION ( 'NONE',  ( 1.000000000000000000, 0.000000000000000000, 0.000000000000000000 ) ) ;
#15615=TOROIDAL_SURFACE ( 'NONE', #18604, 5.633200000000004870, 0.02570000000000859444 ) ;
#15765=DIRECTION ( 'NONE',  ( 0.000000000000000000, 0.000000000000000000, -1.000000000000000000 ) ) ;
#15793=DIRECTION ( 'NONE',  ( 1.000000000000000000, 0.000000000000000000, 0.000000000000000000 ) ) ;
#15803=TOROIDAL_SURFACE ( 'NONE', #22814, 5.100000000000000533, 0.1000000000000005884 ) ;
#15810=CARTESIAN_POINT ( 'NONE',  ( 1.399999999999999467, 0.000000000000000000, -5.100000000000000533 ) ) ;
#15813=ORIENTED_EDGE ( 'NONE', *, *, #45775, .T. ) ;
#15859=STYLED_ITEM ( 'NONE', ( #58210 ), #10859 ) ;
#15868=DIRECTION ( 'NONE',  ( 0.000000000000000000, 0.000000000000000000, -1.000000000000000000 ) ) ;
#15869=CARTESIAN_POINT ( 'NONE',  ( 1.500000000000001332, 6.678152076600409922E-16, -5.453125000000000000 ) ) ;
#15885=CARTESIAN_POINT ( 'NONE',  ( -1.500000000000001332, 9.123618653647808769E-16, 7.400000000000021672 ) ) ;
#15891=CARTESIAN_POINT ( 'NONE',  ( -1.399999999999998579, 0.000000000000000000, -7.500000000000022204 ) ) ;
#15915=EDGE_LOOP ( 'NONE', ( #19346, #56273, #35497, #14869 ) ) ;
#16018=LINE ( 'NONE', #59518, #8330 ) ;
#16050=DIRECTION ( 'NONE',  ( 1.000000000000000000, -0.000000000000000000, -0.000000000000000000 ) ) ;
#16097=DIRECTION ( 'NONE',  ( -0.000000000000000000, -1.000000000000000000, -0.000000000000000000 ) ) ;
#16137=ORIENTED_EDGE ( 'NONE', *, *, #14049, .T. ) ;
#16168=DIRECTION ( 'NONE',  ( 1.000000000000000000, 0.000000000000000000, 0.000000000000000000 ) ) ;
#16205=ORIENTED_EDGE ( 'NONE', *, *, #29933, .T. ) ;
#16234=CARTESIAN_POINT ( 'NONE',  ( -1.500000000000001332, 0.000000000000000000, -7.400000000000021672 ) ) ;
#16285=ORIENTED_EDGE ( 'NONE', *, *, #19201, .T. ) ;
#16291=DIRECTION ( 'NONE',  ( 0.000000000000000000, 0.000000000000000000, 1.000000000000000000 ) ) ;
#16324=CIRCLE ( 'NONE', #56329, 0.02570000000000870199 ) ;
#16422=ADVANCED_FACE ( 'NONE', ( #17322 ), #7271, .F. ) ;
#16434=ORIENTED_EDGE ( 'NONE', *, *, #32514, .T. ) ;
#16477=AXIS2_PLACEMENT_3D ( 'NONE', #59149, #9458, #30644 ) ;
#16483=ORIENTED_EDGE ( 'NONE', *, *, #25181, .T. ) ;
#16578=ADVANCED_FACE ( 'NONE', ( #28251 ), #23251, .F. ) ;
#16605=DIRECTION ( 'NONE',  ( 1.000000000000000000, -0.000000000000000000, -0.000000000000000000 ) ) ;
#16691=DIRECTION ( 'NONE',  ( 0.000000000000000000, 0.000000000000000000, 1.000000000000000000 ) ) ;
#16702=AXIS2_PLACEMENT_3D ( 'NONE', #20638, #54430, #39155 ) ;
#16770=CARTESIAN_POINT ( 'NONE',  ( -1.400000000000000355, 0.000000000000000000, -5.100000000000000533 ) ) ;
#16797=AXIS2_PLACEMENT_3D ( 'NONE', #10851, #24948, #29943 ) ;
#16850=ORIENTED_EDGE ( 'NONE', *, *, #6384, .F. ) ;
#17024=DIRECTION ( 'NONE',  ( 1.000000000000000000, 0.000000000000000000, 0.000000000000000000 ) ) ;
#17045=EDGE_LOOP ( 'NONE', ( #44266, #31686 ) ) ;
#17110=ORIENTED_EDGE ( 'NONE', *, *, #13492, .F. ) ;
#17129=CARTESIAN_POINT ( 'NONE',  ( 1.500000000000001332, 6.775741118407465085E-16, -5.453125000000000000 ) ) ;
#17183=DIRECTION ( 'NONE',  ( 1.000000000000000000, -0.000000000000000000, -0.000000000000000000 ) ) ;
#17252=( NAMED_UNIT ( * ) SI_UNIT ( $, .STERADIAN. ) SOLID_ANGLE_UNIT ( ) );
#17286=EDGE_LOOP ( 'NONE', ( #16483, #61670 ) ) ;
#17320=AXIS2_PLACEMENT_3D ( 'NONE', #12660, #31755, #36469 ) ;
#17322=FACE_OUTER_BOUND ( 'NONE', #11951, .T. ) ;
#17348=AXIS2_PLACEMENT_3D ( 'NONE', #41009, #31891, #36290 ) ;
#17400=AXIS2_PLACEMENT_3D ( 'NONE', #22830, #38491, #51631 ) ;
#17463=DIRECTION ( 'NONE',  ( 0.000000000000000000, -1.000000000000000000, 0.000000000000000000 ) ) ;
#17486=DIRECTION ( 'NONE',  ( -0.000000000000000000, -1.000000000000000000, -0.000000000000000000 ) ) ;
#17524=CIRCLE ( 'NONE', #40529, 0.1000000000000002554 ) ;
#17576=CARTESIAN_POINT ( 'NONE',  ( 1.500000000000001332, 0.000000000000000000, 0.000000000000000000 ) ) ;
#17639=CARTESIAN_POINT ( 'NONE',  ( 1.129531546211701931, 0.000000000000000000, -6.887500000000022382 ) ) ;
#17675=CARTESIAN_POINT ( 'NONE',  ( -1.200000000000006617, 0.000000000000000000, -6.887500000000022382 ) ) ;
#17772=DIRECTION ( 'NONE',  ( 0.000000000000000000, 0.000000000000000000, -1.000000000000000000 ) ) ;
#17845=AXIS2_PLACEMENT_3D ( 'NONE', #46939, #19344, #14652 ) ;
#17863=ORIENTED_EDGE ( 'NONE', *, *, #52684, .T. ) ;
#17879=( GEOMETRIC_REPRESENTATION_CONTEXT ( 3 ) GLOBAL_UNCERTAINTY_ASSIGNED_CONTEXT ( ( #31127 ) ) GLOBAL_UNIT_ASSIGNED_CONTEXT ( ( #1204, #30331, #49443 ) ) REPRESENTATION_CONTEXT ( 'NONE', 'WORKASPACE' ) );
#17905=ADVANCED_FACE ( 'NONE', ( #40835, #21385 ), #40518, .T. ) ;
#17916=ORIENTED_EDGE ( 'NONE', *, *, #33544, .T. ) ;
#17962=CARTESIAN_POINT ( 'NONE',  ( 1.114299999999999846, 0.000000000000000000, -5.633200000000004870 ) ) ;
#18114=CIRCLE ( 'NONE', #53104, 6.887500000000022382 ) ;
#18228=DIRECTION ( 'NONE',  ( 1.000000000000000000, -0.000000000000000000, -0.000000000000000000 ) ) ;
#18248=AXIS2_PLACEMENT_3D ( 'NONE', #49291, #6347, #25483 ) ;
#18293=VECTOR ( 'NONE', #35454, 1000.000000000000000 ) ;
#18381=PLANE ( 'NONE',  #50996 ) ;
#18417=DIRECTION ( 'NONE',  ( 0.000000000000000000, 0.000000000000000000, -1.000000000000000000 ) ) ;
#18460=DIRECTION ( 'NONE',  ( 1.000000000000000000, -0.000000000000000000, -0.000000000000000000 ) ) ;
#18478=( LENGTH_UNIT ( ) NAMED_UNIT ( * ) SI_UNIT ( .MILLI., .METRE. ) );
#18481=CARTESIAN_POINT ( 'NONE',  ( -1.500000000000001332, 6.775741118407465085E-16, 5.453125000000000000 ) ) ;
#18511=EDGE_LOOP ( 'NONE', ( #5495, #30502, #42483, #24901 ) ) ;
#18604=AXIS2_PLACEMENT_3D ( 'NONE', #38111, #47182, #4532 ) ;
#18647=FACE_OUTER_BOUND ( 'NONE', #56049, .T. ) ;
#18673=FACE_OUTER_BOUND ( 'NONE', #32170, .T. ) ;
#18725=ADVANCED_FACE ( 'NONE', ( #27788 ), #4882, .T. ) ;
#18748=EDGE_CURVE ( 'NONE', #32528, #30513, #18808, .T. ) ;
#18751=DIRECTION ( 'NONE',  ( 0.000000000000000000, 0.000000000000000000, -1.000000000000000000 ) ) ;
#18754=AXIS2_PLACEMENT_3D ( 'NONE', #35704, #30981, #45108 ) ;
#18808=CIRCLE ( 'NONE', #22773, 5.633200000000004870 ) ;
#18823=EDGE_CURVE ( 'NONE', #58899, #23453, #29790, .T. ) ;
#18877=AXIS2_PLACEMENT_3D ( 'NONE', #2073, #58164, #40044 ) ;
#19106=ORIENTED_EDGE ( 'NONE', *, *, #27858, .F. ) ;
#19121=LINE ( 'NONE', #33832, #41884 ) ;
#19196=AXIS2_PLACEMENT_3D ( 'NONE', #23052, #3600, #32143 ) ;
#19201=EDGE_CURVE ( 'NONE', #19843, #20243, #15168, .T. ) ;
#19209=UNCERTAINTY_MEASURE_WITH_UNIT (LENGTH_MEASURE( 1.000000000000000082E-05 ), #60142, 'distance_accuracy_value', 'NONE');
#19238=AXIS2_PLACEMENT_3D ( 'NONE', #8515, #60514, #52052 ) ;
#19251=DIRECTION ( 'NONE',  ( 1.000000000000000000, 0.000000000000000000, 0.000000000000000000 ) ) ;
#19317=TOROIDAL_SURFACE ( 'NONE', #1267, 6.866799999999992465, 0.02570000000000187065 ) ;
#19318=ORIENTED_EDGE ( 'NONE', *, *, #35408, .T. ) ;
#19340=DIRECTION ( 'NONE',  ( 1.000000000000000000, 0.000000000000000000, 0.000000000000000000 ) ) ;
#19344=DIRECTION ( 'NONE',  ( -0.000000000000000000, -1.000000000000000000, -0.000000000000000000 ) ) ;
#19346=ORIENTED_EDGE ( 'NONE', *, *, #29135, .T. ) ;
#19387=FACE_OUTER_BOUND ( 'NONE', #29116, .T. ) ;
#19441=ORIENTED_EDGE ( 'NONE', *, *, #10565, .T. ) ;
#19512=VERTEX_POINT ( 'NONE', #8677 ) ;
#19545=CIRCLE ( 'NONE', #47577, 6.728125000000023448 ) ;
#19582=ORIENTED_EDGE ( 'NONE', *, *, #50750, .F. ) ;
#19653=CIRCLE ( 'NONE', #52621, 0.02570000000000870199 ) ;
#19754=CARTESIAN_POINT ( 'NONE',  ( 1.500000000000001332, 0.000000000000000000, 0.000000000000000000 ) ) ;
#19773=CIRCLE ( 'NONE', #11771, 6.728125000000023448 ) ;
#19797=CARTESIAN_POINT ( 'NONE',  ( -1.200000000000006617, 0.000000000000000000, 0.000000000000000000 ) ) ;
#19798=AXIS2_PLACEMENT_3D ( 'NONE', #43167, #33144, #5217 ) ;
#19806=DIRECTION ( 'NONE',  ( 0.000000000000000000, 0.000000000000000000, -1.000000000000000000 ) ) ;
#19843=VERTEX_POINT ( 'NONE', #18481 ) ;
#19896=ADVANCED_FACE ( 'NONE', ( #49444 ), #20337, .F. ) ;
#19936=PRODUCT_DEFINITION_FORMATION_WITH_SPECIFIED_SOURCE ( 'ANY', '', #36825, .NOT_KNOWN. ) ;
#19938=ORIENTED_EDGE ( 'NONE', *, *, #8512, .T. ) ;
#19964=DIRECTION ( 'NONE',  ( 0.000000000000000000, 0.000000000000000000, -1.000000000000000000 ) ) ;
#20003=DIRECTION ( 'NONE',  ( 1.000000000000000000, 0.000000000000000000, 0.000000000000000000 ) ) ;
#20015=DIRECTION ( 'NONE',  ( -1.000000000000000000, 0.000000000000000000, -0.000000000000000000 ) ) ;
#20016=AXIS2_PLACEMENT_3D ( 'NONE', #11083, #36673, #50443 ) ;
#20120=DIRECTION ( 'NONE',  ( 0.000000000000000000, 0.000000000000000000, 1.000000000000000000 ) ) ;
#20137=FACE_OUTER_BOUND ( 'NONE', #18511, .T. ) ;
#20144=PLANE ( 'NONE',  #36011 ) ;
#20219=VERTEX_POINT ( 'NONE', #5812 ) ;
#20243=VERTEX_POINT ( 'NONE', #1132 ) ;
#20283=ORIENTED_EDGE ( 'NONE', *, *, #37597, .F. ) ;
#20318=CARTESIAN_POINT ( 'NONE',  ( -1.200000000000006617, 0.000000000000000000, 0.000000000000000000 ) ) ;
#20325=AXIS2_PLACEMENT_3D ( 'NONE', #15810, #58374, #44036 ) ;
#20337=CYLINDRICAL_SURFACE ( 'NONE', #16702, 5.000000000000000888 ) ;
#20385=FACE_OUTER_BOUND ( 'NONE', #15915, .T. ) ;
#20421=ORIENTED_EDGE ( 'NONE', *, *, #3250, .T. ) ;
#20440=CARTESIAN_POINT ( 'NONE',  ( 1.499999999999998668, 7.400000000000022560, 0.000000000000000000 ) ) ;
#20455=AXIS2_PLACEMENT_3D ( 'NONE', #14491, #48002, #35072 ) ;
#20481=CIRCLE ( 'NONE', #55477, 7.400000000000022560 ) ;
#20539=PLANE ( 'NONE',  #10646 ) ;
#20560=DIRECTION ( 'NONE',  ( -0.8831157194574164038, 5.745494457772962184E-17, -0.4691552259617384202 ) ) ;
#20565=CIRCLE ( 'NONE', #30506, 5.612499999999999822 ) ;
#20621=ORIENTED_EDGE ( 'NONE', *, *, #13447, .F. ) ;
#20638=CARTESIAN_POINT ( 'NONE',  ( -90.00000000000000000, 0.000000000000000000, 0.000000000000000000 ) ) ;
#20749=ADVANCED_FACE ( 'NONE', ( #10952 ), #49765, .F. ) ;
#20809=EDGE_CURVE ( 'NONE', #58899, #39657, #55451, .T. ) ;
#20938=DIRECTION ( 'NONE',  ( 1.000000000000000000, 0.000000000000000000, 0.000000000000000000 ) ) ;
#20963=ORIENTED_EDGE ( 'NONE', *, *, #52684, .F. ) ;
#21245=VERTEX_POINT ( 'NONE', #15885 ) ;
#21338=AXIS2_PLACEMENT_3D ( 'NONE', #27964, #42093, #8853 ) ;
#21340=CARTESIAN_POINT ( 'NONE',  ( -90.00000000000000000, 8.239576745513314221E-16, 6.728125000000023448 ) ) ;
#21357=ORIENTED_EDGE ( 'NONE', *, *, #7100, .F. ) ;
#21370=DIRECTION ( 'NONE',  ( 0.000000000000000000, 0.000000000000000000, -1.000000000000000000 ) ) ;
#21385=FACE_OUTER_BOUND ( 'NONE', #54089, .T. ) ;
#21404=DIRECTION ( 'NONE',  ( 0.000000000000000000, 0.000000000000000000, -1.000000000000000000 ) ) ;
#21425=ORIENTED_EDGE ( 'NONE', *, *, #6996, .F. ) ;
#21457=DIRECTION ( 'NONE',  ( 0.000000000000000000, 0.000000000000000000, -1.000000000000000000 ) ) ;
#21515=EDGE_CURVE ( 'NONE', #39657, #8473, #46541, .T. ) ;
#21553=FACE_OUTER_BOUND ( 'NONE', #34958, .T. ) ;
#21616=CYLINDRICAL_SURFACE ( 'NONE', #55889, 7.500000000000022204 ) ;
#21638=EDGE_CURVE ( 'NONE', #45810, #10577, #33344, .T. ) ;
#21661=ORIENTED_EDGE ( 'NONE', *, *, #18748, .T. ) ;
#21709=CARTESIAN_POINT ( 'NONE',  ( -1.200000000000006617, 0.000000000000000000, -5.612499999999999822 ) ) ;
#21773=TOROIDAL_SURFACE ( 'NONE', #1759, 5.100000000000000533, 0.09999999999999982514 ) ;
#21778=PRODUCT_DEFINITION_SHAPE ( 'NONE', 'NONE',  #40600 ) ;
#21849=ORIENTED_EDGE ( 'NONE', *, *, #32543, .T. ) ;
#21886=CARTESIAN_POINT ( 'NONE',  ( -1.500000000000001332, 0.000000000000000000, 0.000000000000000000 ) ) ;
#21893=DIRECTION ( 'NONE',  ( 1.000000000000000000, 0.000000000000000000, 0.000000000000000000 ) ) ;
#21907=CARTESIAN_POINT ( 'NONE',  ( 1.500000000000001332, 0.000000000000000000, 0.000000000000000000 ) ) ;
#21946=DIRECTION ( 'NONE',  ( 1.000000000000000000, 0.000000000000000000, 0.000000000000000000 ) ) ;
#21950=AXIS2_PLACEMENT_3D ( 'NONE', #38867, #4986, #57921 ) ;
#21970=CARTESIAN_POINT ( 'NONE',  ( -1.399999999999998579, 6.184466335694134054E-16, 5.000000000000000000 ) ) ;
#21989=ORIENTED_EDGE ( 'NONE', *, *, #30896, .F. ) ;
#22041=EDGE_LOOP ( 'NONE', ( #5003, #30018, #52197, #21425 ) ) ;
#22147=VERTEX_POINT ( 'NONE', #61084 ) ;
#22266=DIRECTION ( 'NONE',  ( 1.000000000000000000, 0.000000000000000000, 0.000000000000000000 ) ) ;
#22308=ORIENTED_EDGE ( 'NONE', *, *, #30909, .F. ) ;
#22319=ORIENTED_EDGE ( 'NONE', *, *, #30946, .F. ) ;
#22453=DIRECTION ( 'NONE',  ( 0.000000000000000000, 0.000000000000000000, -1.000000000000000000 ) ) ;
#22558=ADVANCED_FACE ( 'NONE', ( #10187 ), #29775, .T. ) ;
#22573=CARTESIAN_POINT ( 'NONE',  ( 1.140000000000008784, 6.898680348956876061E-16, 5.633200000000004870 ) ) ;
#22579=CARTESIAN_POINT ( 'NONE',  ( -90.00000000000000000, 9.184850993605177527E-16, 7.500000000000022204 ) ) ;
#22630=AXIS2_PLACEMENT_3D ( 'NONE', #19754, #29438, #5916 ) ;
#22666=CIRCLE ( 'NONE', #30651, 5.000000000000000000 ) ;
#22676=CARTESIAN_POINT ( 'NONE',  ( 1.399999999999998579, 0.000000000000000000, -7.500000000000022204 ) ) ;
#22710=COLOUR_RGB ( '', 0.40784314, 0.44705882, 0.49803922) ;
#22747=AXIS2_PLACEMENT_3D ( 'NONE', #44268, #16050, #5678 ) ;
#22753=DIRECTION ( 'NONE',  ( 0.000000000000000000, 0.000000000000000000, -1.000000000000000000 ) ) ;
#22758=EDGE_CURVE ( 'NONE', #60897, #61018, #31986, .T. ) ;
#22773=AXIS2_PLACEMENT_3D ( 'NONE', #58122, #2031, #39995 ) ;
#22775=VERTEX_POINT ( 'NONE', #22983 ) ;
#22782=AXIS2_PLACEMENT_3D ( 'NONE', #43404, #8613, #47469 ) ;
#22814=AXIS2_PLACEMENT_3D ( 'NONE', #5340, #53274, #10388 ) ;
#22821=DIRECTION ( 'NONE',  ( 1.000000000000000000, 0.000000000000000000, 0.000000000000000000 ) ) ;
#22830=CARTESIAN_POINT ( 'NONE',  ( -1.114299999999999624, 8.409404640385035208E-16, 6.866799999999992465 ) ) ;
#22839=ORIENTED_EDGE ( 'NONE', *, *, #33544, .F. ) ;
#22968=ORIENTED_EDGE ( 'NONE', *, *, #24500, .T. ) ;
#22983=CARTESIAN_POINT ( 'NONE',  ( 1.399999999999998579, 9.184850993605177527E-16, 7.500000000000022204 ) ) ;
#23052=CARTESIAN_POINT ( 'NONE',  ( -90.00000000000000000, 0.000000000000000000, 0.000000000000000000 ) ) ;
#23077=FACE_OUTER_BOUND ( 'NONE', #277, .T. ) ;
#23177=FILL_AREA_STYLE ('',( #4037 ) ) ;
#23178=DIRECTION ( 'NONE',  ( 0.000000000000000000, 0.000000000000000000, -1.000000000000000000 ) ) ;
#23251=CYLINDRICAL_SURFACE ( 'NONE', #19238, 6.728125000000023448 ) ;
#23255=DIRECTION ( 'NONE',  ( 0.000000000000000000, 0.000000000000000000, -1.000000000000000000 ) ) ;
#23307=VERTEX_POINT ( 'NONE', #30947 ) ;
#23399=DIRECTION ( 'NONE',  ( 0.000000000000000000, 0.000000000000000000, -1.000000000000000000 ) ) ;
#23453=VERTEX_POINT ( 'NONE', #37520 ) ;
#23459=CARTESIAN_POINT ( 'NONE',  ( -90.00000000000000000, 0.000000000000000000, -5.000000000000000888 ) ) ;
#23524=ORIENTED_EDGE ( 'NONE', *, *, #43626, .F. ) ;
#23691=ORIENTED_EDGE ( 'NONE', *, *, #18748, .F. ) ;
#23737=CIRCLE ( 'NONE', #34748, 0.1000000000000002554 ) ;
#23855=CARTESIAN_POINT ( 'NONE',  ( -90.00000000000000000, 0.000000000000000000, 0.000000000000000000 ) ) ;
#23885=CARTESIAN_POINT ( 'NONE',  ( 1.500000000000001332, 0.000000000000000000, 0.000000000000000000 ) ) ;
#23913=CIRCLE ( 'NONE', #58910, 6.887500000000022382 ) ;
#23919=EDGE_CURVE ( 'NONE', #20243, #1725, #12017, .T. ) ;
#23932=VERTEX_POINT ( 'NONE', #58655 ) ;
#23963=AXIS2_PLACEMENT_3D ( 'NONE', #42563, #22821, #18751 ) ;
#24139=CARTESIAN_POINT ( 'NONE',  ( 1.399999999999998579, 0.000000000000000000, -5.000000000000000888 ) ) ;
#24171=CARTESIAN_POINT ( 'NONE',  ( -1.129531546211690163, 0.000000000000000000, 0.000000000000000000 ) ) ;
#24216=CARTESIAN_POINT ( 'NONE',  ( -1.200000000000006617, 0.000000000000000000, 0.000000000000000000 ) ) ;
#24335=CARTESIAN_POINT ( 'NONE',  ( -1.400000000000000799, 0.000000000000000000, 0.000000000000000000 ) ) ;
#24374=AXIS2_PLACEMENT_3D ( 'NONE', #44136, #20003, #1164 ) ;
#24379=ORIENTED_EDGE ( 'NONE', *, *, #45775, .F. ) ;
#24500=EDGE_CURVE ( 'NONE', #15229, #19843, #30003, .T. ) ;
#24528=EDGE_LOOP ( 'NONE', ( #2676, #55037 ) ) ;
#24631=CARTESIAN_POINT ( 'NONE',  ( 1.139999999999998570, 0.000000000000000000, 0.000000000000000000 ) ) ;
#24719=( NAMED_UNIT ( * ) SI_UNIT ( $, .STERADIAN. ) SOLID_ANGLE_UNIT ( ) );
#24730=EDGE_LOOP ( 'NONE', ( #22319, #42706, #3942, #44333 ) ) ;
#24783=DIRECTION ( 'NONE',  ( 0.000000000000000000, 0.000000000000000000, -1.000000000000000000 ) ) ;
#24848=CYLINDRICAL_SURFACE ( 'NONE', #54469, 6.887500000000022382 ) ;
#24901=ORIENTED_EDGE ( 'NONE', *, *, #14049, .F. ) ;
#24935=ORIENTED_EDGE ( 'NONE', *, *, #36296, .F. ) ;
#24948=DIRECTION ( 'NONE',  ( 0.000000000000000000, 1.000000000000000000, -1.224646799147353207E-16 ) ) ;
#24992=AXIS2_PLACEMENT_3D ( 'NONE', #9640, #15593, #29363 ) ;
#25010=ORIENTED_EDGE ( 'NONE', *, *, #14362, .F. ) ;
#25031=FILL_AREA_STYLE_COLOUR ( '', #58843 ) ;
#25110=FACE_OUTER_BOUND ( 'NONE', #41644, .T. ) ;
#25119=VERTEX_POINT ( 'NONE', #26337 ) ;
#25181=EDGE_CURVE ( 'NONE', #1177, #23932, #57042, .T. ) ;
#25182=CARTESIAN_POINT ( 'NONE',  ( -1.139999999999999902, 0.000000000000000000, -5.633200000000004870 ) ) ;
#25197=VERTEX_POINT ( 'NONE', #22573 ) ;
#25246=EDGE_CURVE ( 'NONE', #48814, #25197, #29028, .T. ) ;
#25302=DIRECTION ( 'NONE',  ( -0.000000000000000000, 0.000000000000000000, 1.000000000000000000 ) ) ;
#25372=DIRECTION ( 'NONE',  ( 0.000000000000000000, 0.000000000000000000, -1.000000000000000000 ) ) ;
#25467=VECTOR ( 'NONE', #37971, 1000.000000000000000 ) ;
#25475=CIRCLE ( 'NONE', #30435, 5.453125000000000000 ) ;
#25483=DIRECTION ( 'NONE',  ( 0.000000000000000000, 0.000000000000000000, -1.000000000000000000 ) ) ;
#25511=ORIENTED_EDGE ( 'NONE', *, *, #50476, .F. ) ;
#25578=ORIENTED_EDGE ( 'NONE', *, *, #43194, .T. ) ;
#25611=CARTESIAN_POINT ( 'NONE',  ( -1.500000000000000444, 5.453125000000000000, 0.000000000000000000 ) ) ;
#25613=CONICAL_SURFACE ( 'NONE', #9645, 5.612499999999999822, 0.4883339510564123076 ) ;
#25619=AXIS2_PLACEMENT_3D ( 'NONE', #24335, #43466, #19964 ) ;
#25674=ORIENTED_EDGE ( 'NONE', *, *, #20809, .F. ) ;
#25757=VERTEX_POINT ( 'NONE', #37588 ) ;
#25837=ADVANCED_FACE ( 'NONE', ( #26936 ), #61024, .T. ) ;
#25900=ORIENTED_EDGE ( 'NONE', *, *, #44539, .T. ) ;
#25928=AXIS2_PLACEMENT_3D ( 'NONE', #39594, #39284, #403 ) ;
#25959=ADVANCED_FACE ( 'NONE', ( #42588 ), #45064, .T. ) ;
#25967=EDGE_CURVE ( 'NONE', #43343, #47186, #42071, .T. ) ;
#26012=DIRECTION ( 'NONE',  ( 0.000000000000000000, 0.000000000000000000, -1.000000000000000000 ) ) ;
#26191=CIRCLE ( 'NONE', #4121, 7.500000000000022204 ) ;
#26207=ORIENTED_EDGE ( 'NONE', *, *, #2519, .F. ) ;
#26337=CARTESIAN_POINT ( 'NONE',  ( -1.129531546211690163, 0.000000000000000000, -6.887500000000022382 ) ) ;
#26385=VERTEX_POINT ( 'NONE', #35584 ) ;
#26449=ORIENTED_EDGE ( 'NONE', *, *, #20809, .T. ) ;
#26548=DIRECTION ( 'NONE',  ( 0.000000000000000000, 0.000000000000000000, -1.000000000000000000 ) ) ;
#26628=EDGE_LOOP ( 'NONE', ( #34170, #28999, #61329, #4153 ) ) ;
#26630=ORIENTED_EDGE ( 'NONE', *, *, #58243, .F. ) ;
#26634=SURFACE_SIDE_STYLE ('',( #37604 ) ) ;
#26646=DIRECTION ( 'NONE',  ( 1.000000000000000000, -0.000000000000000000, -0.000000000000000000 ) ) ;
#26848=CIRCLE ( 'NONE', #37881, 6.866799999999992465 ) ;
#26870=VECTOR ( 'NONE', #54026, 1000.000000000000000 ) ;
#26887=DIRECTION ( 'NONE',  ( 0.000000000000000000, 0.000000000000000000, -1.000000000000000000 ) ) ;
#26936=FACE_OUTER_BOUND ( 'NONE', #31295, .T. ) ;
#26964=DIRECTION ( 'NONE',  ( 0.000000000000000000, 0.000000000000000000, -1.000000000000000000 ) ) ;
#27016=ADVANCED_FACE ( 'NONE', ( #59440 ), #806, .T. ) ;
#27034=DIRECTION ( 'NONE',  ( 0.000000000000000000, 1.224646799147331020E-16, 1.000000000000000000 ) ) ;
#27065=ADVANCED_FACE ( 'NONE', ( #21553 ), #15803, .T. ) ;
#27160=ADVANCED_FACE ( 'NONE', ( #3345 ), #51819, .T. ) ;
#27190=CARTESIAN_POINT ( 'NONE',  ( -1.139999999999998570, 0.000000000000000000, 0.000000000000000000 ) ) ;
#27235=EDGE_CURVE ( 'NONE', #60897, #25119, #43778, .T. ) ;
#27242=CARTESIAN_POINT ( 'NONE',  ( 1.114300000000000068, 0.000000000000000000, 0.000000000000000000 ) ) ;
#27308=CIRCLE ( 'NONE', #42359, 5.100000000000000533 ) ;
#27368=DIRECTION ( 'NONE',  ( 0.000000000000000000, 0.000000000000000000, -1.000000000000000000 ) ) ;
#27416=ORIENTED_EDGE ( 'NONE', *, *, #11911, .T. ) ;
#27489=DIRECTION ( 'NONE',  ( 0.000000000000000000, 0.000000000000000000, -1.000000000000000000 ) ) ;
#27521=DIRECTION ( 'NONE',  ( -1.000000000000000000, 0.000000000000000000, 0.000000000000000000 ) ) ;
#27537=CARTESIAN_POINT ( 'NONE',  ( 1.500000000000000444, 0.000000000000000000, -5.100000000000000533 ) ) ;
#27554=ADVANCED_FACE ( 'NONE', ( #52127, #4191 ), #28948, .T. ) ;
#27561=CARTESIAN_POINT ( 'NONE',  ( -1.400000000000000355, 6.245698675651501825E-16, 5.100000000000000533 ) ) ;
#27602=DIRECTION ( 'NONE',  ( 0.000000000000000000, 1.000000000000000000, -1.224646799147353207E-16 ) ) ;
#27678=EDGE_LOOP ( 'NONE', ( #30605, #207 ) ) ;
#27685=CIRCLE ( 'NONE', #47678, 0.02570000000000870199 ) ;
#27748=CIRCLE ( 'NONE', #36897, 5.453125000000000000 ) ;
#27769=CARTESIAN_POINT ( 'NONE',  ( 1.500000000000001332, 8.239576745513314221E-16, 6.728125000000023448 ) ) ;
#27788=FACE_OUTER_BOUND ( 'NONE', #36640, .T. ) ;
#27858=EDGE_CURVE ( 'NONE', #15229, #1725, #55513, .T. ) ;
#27912=ORIENTED_EDGE ( 'NONE', *, *, #52261, .F. ) ;
#27964=CARTESIAN_POINT ( 'NONE',  ( -90.00000000000000000, 0.000000000000000000, 0.000000000000000000 ) ) ;
#28066=AXIS2_PLACEMENT_3D ( 'NONE', #45628, #40950, #45027 ) ;
#28175=SHAPE_REPRESENTATION_RELATIONSHIP ( 'NONE' , 'NONE' ,  #40484, #59429 ) ;
#28192=DIRECTION ( 'NONE',  ( 1.000000000000000000, 0.000000000000000000, 0.000000000000000000 ) ) ;
#28196=FACE_OUTER_BOUND ( 'NONE', #44820, .T. ) ;
#28238=DIRECTION ( 'NONE',  ( 1.000000000000000000, 0.000000000000000000, 0.000000000000000000 ) ) ;
#28251=FACE_OUTER_BOUND ( 'NONE', #22041, .T. ) ;
#28282=EDGE_CURVE ( 'NONE', #1725, #14527, #19121, .T. ) ;
#28340=DIRECTION ( 'NONE',  ( 1.000000000000000000, 0.000000000000000000, 0.000000000000000000 ) ) ;
#28346=CARTESIAN_POINT ( 'NONE',  ( 1.399999999999998579, 0.000000000000000000, 0.000000000000000000 ) ) ;
#28615=CIRCLE ( 'NONE', #11643, 6.887500000000022382 ) ;
#28729=DIRECTION ( 'NONE',  ( 0.000000000000000000, 0.000000000000000000, -1.000000000000000000 ) ) ;
#28791=CARTESIAN_POINT ( 'NONE',  ( 1.140000000000009006, 0.000000000000000000, 0.000000000000000000 ) ) ;
#28801=ADVANCED_FACE ( 'NONE', ( #20385 ), #21616, .T. ) ;
#28859=ORIENTED_EDGE ( 'NONE', *, *, #2519, .T. ) ;
#28873=EDGE_CURVE ( 'NONE', #36274, #48937, #55112, .T. ) ;
#28948=PLANE ( 'NONE',  #51861 ) ;
#28999=ORIENTED_EDGE ( 'NONE', *, *, #52664, .T. ) ;
#29028=CIRCLE ( 'NONE', #55030, 5.633200000000004870 ) ;
#29030=DIRECTION ( 'NONE',  ( 1.000000000000000000, 0.000000000000000000, 0.000000000000000000 ) ) ;
#29116=EDGE_LOOP ( 'NONE', ( #43949, #3220, #35650, #27912 ) ) ;
#29135=EDGE_CURVE ( 'NONE', #31646, #8175, #45956, .T. ) ;
#29167=DIRECTION ( 'NONE',  ( 1.000000000000000000, 0.000000000000000000, 0.000000000000000000 ) ) ;
#29181=DIRECTION ( 'NONE',  ( 0.000000000000000000, 0.000000000000000000, -1.000000000000000000 ) ) ;
#29275=TOROIDAL_SURFACE ( 'NONE', #14280, 6.866799999999992465, 0.02570000000000187065 ) ;
#29363=DIRECTION ( 'NONE',  ( 0.000000000000000000, 0.000000000000000000, -1.000000000000000000 ) ) ;
#29400=ORIENTED_EDGE ( 'NONE', *, *, #39412, .F. ) ;
#29428=VERTEX_POINT ( 'NONE', #4808 ) ;
#29430=FACE_BOUND ( 'NONE', #39313, .T. ) ;
#29438=DIRECTION ( 'NONE',  ( 1.000000000000000000, 0.000000000000000000, 0.000000000000000000 ) ) ;
#29496=EDGE_LOOP ( 'NONE', ( #13052, #16205, #10817, #46638 ) ) ;
#29597=AXIS2_PLACEMENT_3D ( 'NONE', #19797, #34510, #5647 ) ;
#29775=CONICAL_SURFACE ( 'NONE', #4277, 5.612499999999999822, 0.4883339510564123076 ) ;
#29784=DIRECTION ( 'NONE',  ( 0.000000000000000000, 0.000000000000000000, -1.000000000000000000 ) ) ;
#29790=CIRCLE ( 'NONE', #16797, 0.09999999999999939493 ) ;
#29825=CYLINDRICAL_SURFACE ( 'NONE', #47097, 6.887500000000022382 ) ;
#29933=EDGE_CURVE ( 'NONE', #23932, #43343, #30718, .T. ) ;
#29943=DIRECTION ( 'NONE',  ( 0.000000000000000000, 1.224646799147353947E-16, 1.000000000000000000 ) ) ;
#29986=TOROIDAL_SURFACE ( 'NONE', #23963, 7.400000000000022560, 0.09999999999999961697 ) ;
#29998=CARTESIAN_POINT ( 'NONE',  ( -1.399999999999998579, 0.000000000000000000, 0.000000000000000000 ) ) ;
#30003=CIRCLE ( 'NONE', #57975, 5.453125000000000000 ) ;
#30018=ORIENTED_EDGE ( 'NONE', *, *, #30946, .T. ) ;
#30070=ORIENTED_EDGE ( 'NONE', *, *, #49649, .F. ) ;
#30113=DIRECTION ( 'NONE',  ( -1.000000000000000000, -0.000000000000000000, -0.000000000000000000 ) ) ;
#30331=( NAMED_UNIT ( * ) PLANE_ANGLE_UNIT ( ) SI_UNIT ( $, .RADIAN. ) );
#30415=DIRECTION ( 'NONE',  ( 0.000000000000000000, 0.000000000000000000, -1.000000000000000000 ) ) ;
#30423=PRODUCT_DEFINITION_CONTEXT ( 'detailed design', #50454, 'design' ) ;
#30435=AXIS2_PLACEMENT_3D ( 'NONE', #52651, #29167, #29784 ) ;
#30502=ORIENTED_EDGE ( 'NONE', *, *, #14362, .T. ) ;
#30506=AXIS2_PLACEMENT_3D ( 'NONE', #7788, #27521, #3084 ) ;
#30513=VERTEX_POINT ( 'NONE', #25182 ) ;
#30537=EDGE_CURVE ( 'NONE', #29428, #40414, #2203, .T. ) ;
#30605=ORIENTED_EDGE ( 'NONE', *, *, #56286, .T. ) ;
#30644=DIRECTION ( 'NONE',  ( 0.000000000000000000, 0.000000000000000000, -1.000000000000000000 ) ) ;
#30651=AXIS2_PLACEMENT_3D ( 'NONE', #58125, #16168, #34655 ) ;
#30718=LINE ( 'NONE', #46091, #5202 ) ;
#30727=LINE ( 'NONE', #21340, #18293 ) ;
#30825=CARTESIAN_POINT ( 'NONE',  ( -1.139999999999998570, 0.000000000000000000, 0.000000000000000000 ) ) ;
#30896=EDGE_CURVE ( 'NONE', #8175, #22775, #6902, .T. ) ;
#30909=EDGE_CURVE ( 'NONE', #8473, #23453, #55237, .T. ) ;
#30946=EDGE_CURVE ( 'NONE', #8563, #46275, #30727, .T. ) ;
#30947=CARTESIAN_POINT ( 'NONE',  ( 1.199999999999992628, 8.434754829127421589E-16, 6.887500000000022382 ) ) ;
#30981=DIRECTION ( 'NONE',  ( -1.000000000000000000, 0.000000000000000000, 0.000000000000000000 ) ) ;
#30986=DIRECTION ( 'NONE',  ( 1.000000000000000000, 0.000000000000000000, 0.000000000000000000 ) ) ;
#30988=ADVANCED_FACE ( 'NONE', ( #46707 ), #36981, .F. ) ;
#31004=ORIENTED_EDGE ( 'NONE', *, *, #6384, .T. ) ;
#31020=ADVANCED_FACE ( 'NONE', ( #8777 ), #29275, .T. ) ;
#31127=UNCERTAINTY_MEASURE_WITH_UNIT (LENGTH_MEASURE( 1.000000000000000082E-05 ), #1204, 'distance_accuracy_value', 'NONE');
#31136=EDGE_CURVE ( 'NONE', #11576, #472, #34148, .T. ) ;
#31221=ORIENTED_EDGE ( 'NONE', *, *, #2168, .F. ) ;
#31259=EDGE_CURVE ( 'NONE', #47550, #26385, #27308, .T. ) ;
#31295=EDGE_LOOP ( 'NONE', ( #25010, #11606, #16137, #11497 ) ) ;
#31322=ORIENTED_EDGE ( 'NONE', *, *, #25246, .T. ) ;
#31342=DIRECTION ( 'NONE',  ( 1.000000000000000000, -0.000000000000000000, -0.000000000000000000 ) ) ;
#31519=DIRECTION ( 'NONE',  ( 0.000000000000000000, 0.000000000000000000, -1.000000000000000000 ) ) ;
#31615=CIRCLE ( 'NONE', #22630, 5.453125000000000000 ) ;
#31623=CARTESIAN_POINT ( 'NONE',  ( 1.129531546211701931, 0.000000000000000000, 0.000000000000000000 ) ) ;
#31646=VERTEX_POINT ( 'NONE', #15891 ) ;
#31686=ORIENTED_EDGE ( 'NONE', *, *, #57322, .T. ) ;
#31731=DIRECTION ( 'NONE',  ( 0.8831157194574072999, 0.000000000000000000, -0.4691552259617553511 ) ) ;
#31755=DIRECTION ( 'NONE',  ( 0.000000000000000000, -1.000000000000000000, 0.000000000000000000 ) ) ;
#31818=CARTESIAN_POINT ( 'NONE',  ( 1.114299999999999846, 6.898680348956876061E-16, 5.633200000000004870 ) ) ;
#31887=ORIENTED_EDGE ( 'NONE', *, *, #58243, .T. ) ;
#31891=DIRECTION ( 'NONE',  ( 1.000000000000000000, 0.000000000000000000, 0.000000000000000000 ) ) ;
#31909=ADVANCED_FACE ( 'NONE', ( #4110 ), #19317, .T. ) ;
#31986=CIRCLE ( 'NONE', #50970, 6.887500000000022382 ) ;
#32006=ORIENTED_EDGE ( 'NONE', *, *, #25181, .F. ) ;
#32133=DIRECTION ( 'NONE',  ( 0.000000000000000000, 1.224646799147324364E-16, 1.000000000000000000 ) ) ;
#32143=DIRECTION ( 'NONE',  ( 0.000000000000000000, 0.000000000000000000, -1.000000000000000000 ) ) ;
#32170=EDGE_LOOP ( 'NONE', ( #31322, #53194, #23524, #25511 ) ) ;
#32346=EDGE_CURVE ( 'NONE', #61018, #46714, #16018, .T. ) ;
#32364=DIRECTION ( 'NONE',  ( 0.000000000000000000, 0.000000000000000000, -1.000000000000000000 ) ) ;
#32514=EDGE_CURVE ( 'NONE', #25197, #48814, #15389, .T. ) ;
#32528=VERTEX_POINT ( 'NONE', #10622 ) ;
#32543=EDGE_CURVE ( 'NONE', #22775, #45810, #59351, .T. ) ;
#32657=DIRECTION ( 'NONE',  ( 1.000000000000000000, -0.000000000000000000, -0.000000000000000000 ) ) ;
#32754=DIRECTION ( 'NONE',  ( 0.000000000000000000, 1.000000000000000000, -1.224646799147353207E-16 ) ) ;
#32790=EDGE_CURVE ( 'NONE', #46275, #61755, #39404, .T. ) ;
#32852=EDGE_CURVE ( 'NONE', #22147, #20219, #5197, .T. ) ;
#32922=PLANE ( 'NONE',  #10702 ) ;
#33066=CARTESIAN_POINT ( 'NONE',  ( -90.00000000000000000, 0.000000000000000000, 0.000000000000000000 ) ) ;
#33144=DIRECTION ( 'NONE',  ( 1.000000000000000000, -0.000000000000000000, -0.000000000000000000 ) ) ;
#33157=APPLICATION_CONTEXT ( 'automotive_design' ) ;
#33220=CARTESIAN_POINT ( 'NONE',  ( -1.114299999999999624, 0.000000000000000000, 0.000000000000000000 ) ) ;
#33234=ORIENTED_EDGE ( 'NONE', *, *, #50084, .F. ) ;
#33323=ORIENTED_EDGE ( 'NONE', *, *, #25246, .F. ) ;
#33344=CIRCLE ( 'NONE', #17320, 0.09999999999999939493 ) ;
#33425=AXIS2_PLACEMENT_3D ( 'NONE', #10365, #39197, #43906 ) ;
#33484=ORIENTED_EDGE ( 'NONE', *, *, #7494, .F. ) ;
#33497=DIRECTION ( 'NONE',  ( 1.000000000000000000, 0.000000000000000000, 0.000000000000000000 ) ) ;
#33544=EDGE_CURVE ( 'NONE', #25119, #46714, #10413, .T. ) ;
#33690=DIRECTION ( 'NONE',  ( 1.000000000000000000, 0.000000000000000000, 0.000000000000000000 ) ) ;
#33731=EDGE_LOOP ( 'NONE', ( #47169, #46383, #46815, #25900 ) ) ;
#33832=CARTESIAN_POINT ( 'NONE',  ( -90.00000000000000000, 0.000000000000000000, -5.612499999999999822 ) ) ;
#33843=CARTESIAN_POINT ( 'NONE',  ( -90.00000000000000000, 0.000000000000000000, -6.887500000000022382 ) ) ;
#33870=CARTESIAN_POINT ( 'NONE',  ( -90.00000000000000000, 0.000000000000000000, -6.728125000000023448 ) ) ;
#33996=AXIS2_PLACEMENT_3D ( 'NONE', #30825, #12065, #1688 ) ;
#34148=LINE ( 'NONE', #33843, #4256 ) ;
#34158=DIRECTION ( 'NONE',  ( 1.000000000000000000, 0.000000000000000000, 0.000000000000000000 ) ) ;
#34170=ORIENTED_EDGE ( 'NONE', *, *, #19201, .F. ) ;
#34359=CARTESIAN_POINT ( 'NONE',  ( 1.140000000000008784, 0.000000000000000000, -5.633200000000004870 ) ) ;
#34402=CIRCLE ( 'NONE', #33425, 6.887500000000022382 ) ;
#34510=DIRECTION ( 'NONE',  ( 1.000000000000000000, 0.000000000000000000, 0.000000000000000000 ) ) ;
#34655=DIRECTION ( 'NONE',  ( 0.000000000000000000, 0.000000000000000000, -1.000000000000000000 ) ) ;
#34748=AXIS2_PLACEMENT_3D ( 'NONE', #56093, #27602, #47639 ) ;
#34859=CARTESIAN_POINT ( 'NONE',  ( -90.00000000000000000, 6.873330160214519262E-16, 5.612499999999999822 ) ) ;
#34877=VERTEX_POINT ( 'NONE', #16234 ) ;
#34958=EDGE_LOOP ( 'NONE', ( #51805, #51321, #49166, #5100 ) ) ;
#34987=CARTESIAN_POINT ( 'NONE',  ( -1.500000000000001332, 0.000000000000000000, 0.000000000000000000 ) ) ;
#35072=DIRECTION ( 'NONE',  ( 0.000000000000000000, 0.000000000000000000, -1.000000000000000000 ) ) ;
#35077=AXIS2_PLACEMENT_3D ( 'NONE', #27242, #18460, #8125 ) ;
#35095=CARTESIAN_POINT ( 'NONE',  ( 1.199999999999992628, 0.000000000000000000, 0.000000000000000000 ) ) ;
#35111=ORIENTED_EDGE ( 'NONE', *, *, #41485, .T. ) ;
#35159=EDGE_CURVE ( 'NONE', #37959, #25757, #37220, .T. ) ;
#35175=DIRECTION ( 'NONE',  ( 1.000000000000000000, 0.000000000000000000, 0.000000000000000000 ) ) ;
#35408=EDGE_CURVE ( 'NONE', #8175, #31646, #26191, .T. ) ;
#35416=DIRECTION ( 'NONE',  ( 1.000000000000000000, 0.000000000000000000, 0.000000000000000000 ) ) ;
#35445=DIRECTION ( 'NONE',  ( 0.000000000000000000, 0.000000000000000000, 1.000000000000000000 ) ) ;
#35454=DIRECTION ( 'NONE',  ( 1.000000000000000000, 0.000000000000000000, 0.000000000000000000 ) ) ;
#35497=ORIENTED_EDGE ( 'NONE', *, *, #3250, .F. ) ;
#35584=CARTESIAN_POINT ( 'NONE',  ( -1.500000000000001110, 6.245698675651501825E-16, 5.100000000000000533 ) ) ;
#35650=ORIENTED_EDGE ( 'NONE', *, *, #31259, .F. ) ;
#35704=CARTESIAN_POINT ( 'NONE',  ( -1.129531546211723025, 0.000000000000000000, 0.000000000000000000 ) ) ;
#35783=AXIS2_PLACEMENT_3D ( 'NONE', #24216, #43352, #14227 ) ;
#35957=LINE ( 'NONE', #60038, #61715 ) ;
#36011=AXIS2_PLACEMENT_3D ( 'NONE', #20440, #35175, #21370 ) ;
#36021=DIRECTION ( 'NONE',  ( 0.000000000000000000, 0.000000000000000000, -1.000000000000000000 ) ) ;
#36069=CLOSED_SHELL ( 'NONE', ( #3718, #36467, #16422, #61639, #60637, #18725, #276, #38210, #59742, #61306, #31020, #1033, #16578, #27016, #28801, #56631, #30988, #9182, #40826, #46307, #50832, #40090, #45262, #4261, #45165, #45914, #20749, #5065, #15367, #31909, #17905, #10633, #27160, #27554, #25837, #50435, #11381, #22558, #51888, #27065, #19896, #8520, #13035, #25959 ) ) ;
#36082=CARTESIAN_POINT ( 'NONE',  ( 1.399999999999998579, 0.000000000000000000, 0.000000000000000000 ) ) ;
#36216=DIRECTION ( 'NONE',  ( 0.000000000000000000, 1.224646799147331020E-16, 1.000000000000000000 ) ) ;
#36274=VERTEX_POINT ( 'NONE', #57253 ) ;
#36290=DIRECTION ( 'NONE',  ( 0.000000000000000000, 0.000000000000000000, -1.000000000000000000 ) ) ;
#36296=EDGE_CURVE ( 'NONE', #2066, #8473, #13458, .T. ) ;
#36387=AXIS2_PLACEMENT_3D ( 'NONE', #57136, #32754, #32133 ) ;
#36467=ADVANCED_FACE ( 'NONE', ( #45992 ), #21773, .T. ) ;
#36469=DIRECTION ( 'NONE',  ( 0.000000000000000000, 0.000000000000000000, -1.000000000000000000 ) ) ;
#36470=AXIS2_PLACEMENT_3D ( 'NONE', #16770, #55569, #21457 ) ;
#36587=ORIENTED_EDGE ( 'NONE', *, *, #12252, .F. ) ;
#36632=ORIENTED_EDGE ( 'NONE', *, *, #27235, .T. ) ;
#36640=EDGE_LOOP ( 'NONE', ( #42813, #25578, #36587, #54449 ) ) ;
#36673=DIRECTION ( 'NONE',  ( 1.000000000000000000, 0.000000000000000000, 0.000000000000000000 ) ) ;
#36701=ORIENTED_EDGE ( 'NONE', *, *, #14039, .F. ) ;
#36728=AXIS2_PLACEMENT_3D ( 'NONE', #4949, #58410, #42903 ) ;
#36825=PRODUCT ( 'instrument roller bearing_iso_ISO 1224 - 171015 - R,24,SI,NC,24', 'instrument roller bearing_iso_ISO 1224 - 171015 - R,24,SI,NC,24', '', ( #56220 ) ) ;
#36865=DIRECTION ( 'NONE',  ( 1.000000000000000000, 0.000000000000000000, 0.000000000000000000 ) ) ;
#36897=AXIS2_PLACEMENT_3D ( 'NONE', #37854, #19340, #28729 ) ;
#36981=CYLINDRICAL_SURFACE ( 'NONE', #41288, 6.728125000000022560 ) ;
#37023=CARTESIAN_POINT ( 'NONE',  ( 1.199999999999992628, 0.000000000000000000, -6.728125000000023448 ) ) ;
#37220=CIRCLE ( 'NONE', #47181, 6.866799999999992465 ) ;
#37304=CARTESIAN_POINT ( 'NONE',  ( -90.00000000000000000, 0.000000000000000000, 0.000000000000000000 ) ) ;
#37412=ORIENTED_EDGE ( 'NONE', *, *, #51566, .F. ) ;
#37478=CARTESIAN_POINT ( 'NONE',  ( 1.199999999999992628, 0.000000000000000000, 0.000000000000000000 ) ) ;
#37520=CARTESIAN_POINT ( 'NONE',  ( 1.399999999999998579, 6.123233995736767268E-16, 5.000000000000000888 ) ) ;
#37581=AXIS2_PLACEMENT_3D ( 'NONE', #17576, #11328, #30415 ) ;
#37588=CARTESIAN_POINT ( 'NONE',  ( 1.139999999999998570, 8.422079734756228398E-16, 6.866799999999992465 ) ) ;
#37597=EDGE_CURVE ( 'NONE', #3834, #2066, #22666, .T. ) ;
#37604=SURFACE_STYLE_FILL_AREA ( #23177 ) ;
#37618=DIRECTION ( 'NONE',  ( 0.000000000000000000, 0.000000000000000000, -1.000000000000000000 ) ) ;
#37700=ORIENTED_EDGE ( 'NONE', *, *, #11032, .F. ) ;
#37822=FACE_BOUND ( 'NONE', #39987, .T. ) ;
#37854=CARTESIAN_POINT ( 'NONE',  ( 1.500000000000001332, 0.000000000000000000, 0.000000000000000000 ) ) ;
#37881=AXIS2_PLACEMENT_3D ( 'NONE', #56057, #31342, #3428 ) ;
#37959=VERTEX_POINT ( 'NONE', #44925 ) ;
#37971=DIRECTION ( 'NONE',  ( 1.000000000000000000, 0.000000000000000000, 0.000000000000000000 ) ) ;
#38103=ORIENTED_EDGE ( 'NONE', *, *, #2749, .F. ) ;
#38111=CARTESIAN_POINT ( 'NONE',  ( 1.114299999999999846, 0.000000000000000000, 0.000000000000000000 ) ) ;
#38196=EDGE_LOOP ( 'NONE', ( #41185, #48620, #42556, #53268 ) ) ;
#38210=ADVANCED_FACE ( 'NONE', ( #20137 ), #14759, .T. ) ;
#38250=AXIS2_PLACEMENT_3D ( 'NONE', #40234, #17024, #6960 ) ;
#38363=EDGE_CURVE ( 'NONE', #21245, #8175, #23737, .T. ) ;
#38491=DIRECTION ( 'NONE',  ( 0.000000000000000000, 1.000000000000000000, -1.224646799147353207E-16 ) ) ;
#38529=CARTESIAN_POINT ( 'NONE',  ( -1.200000000000006617, 0.000000000000000000, -5.612499999999999822 ) ) ;
#38638=DIRECTION ( 'NONE',  ( 0.000000000000000000, 0.000000000000000000, -1.000000000000000000 ) ) ;
#38656=CARTESIAN_POINT ( 'NONE',  ( -1.129531546211690163, 8.434754829127421589E-16, 6.887500000000022382 ) ) ;
#38678=DIRECTION ( 'NONE',  ( 0.8831157194574072999, 5.745494457773168027E-17, 0.4691552259617553511 ) ) ;
#38838=CIRCLE ( 'NONE', #40891, 0.1000000000000002554 ) ;
#38851=AXIS2_PLACEMENT_3D ( 'NONE', #45685, #20938, #2735 ) ;
#38867=CARTESIAN_POINT ( 'NONE',  ( 1.199999999999998845, 6.728125000000023448, 0.000000000000000000 ) ) ;
#38879=EDGE_LOOP ( 'NONE', ( #52386, #19441 ) ) ;
#38891=DIRECTION ( 'NONE',  ( 0.000000000000000000, 0.000000000000000000, -1.000000000000000000 ) ) ;
#38934=VECTOR ( 'NONE', #40145, 1000.000000000000000 ) ;
#38957=CARTESIAN_POINT ( 'NONE',  ( -90.00000000000000000, 8.434754829127421589E-16, 6.887500000000022382 ) ) ;
#39000=CARTESIAN_POINT ( 'NONE',  ( -90.00000000000000000, 0.000000000000000000, -7.500000000000022204 ) ) ;
#39027=DIRECTION ( 'NONE',  ( 0.000000000000000000, 0.000000000000000000, -1.000000000000000000 ) ) ;
#39155=DIRECTION ( 'NONE',  ( 0.000000000000000000, 0.000000000000000000, -1.000000000000000000 ) ) ;
#39197=DIRECTION ( 'NONE',  ( 1.000000000000000000, 0.000000000000000000, 0.000000000000000000 ) ) ;
#39274=DIRECTION ( 'NONE',  ( 1.000000000000000000, 0.000000000000000000, 0.000000000000000000 ) ) ;
#39284=DIRECTION ( 'NONE',  ( 1.000000000000000000, -0.000000000000000000, -0.000000000000000000 ) ) ;
#39313=EDGE_LOOP ( 'NONE', ( #40191, #10890 ) ) ;
#39320=ORIENTED_EDGE ( 'NONE', *, *, #2749, .T. ) ;
#39404=CIRCLE ( 'NONE', #17348, 6.728125000000023448 ) ;
#39412=EDGE_CURVE ( 'NONE', #1725, #20243, #56756, .T. ) ;
#39497=ORIENTED_EDGE ( 'NONE', *, *, #13250, .T. ) ;
#39517=CARTESIAN_POINT ( 'NONE',  ( -1.200000000000006617, 0.000000000000000000, -6.728125000000022560 ) ) ;
#39525=CARTESIAN_POINT ( 'NONE',  ( 1.399999999999998579, 0.000000000000000000, 0.000000000000000000 ) ) ;
#39561=EDGE_CURVE ( 'NONE', #11576, #40053, #57647, .T. ) ;
#39594=CARTESIAN_POINT ( 'NONE',  ( 1.129531546211735016, 0.000000000000000000, 0.000000000000000000 ) ) ;
#39657=VERTEX_POINT ( 'NONE', #27537 ) ;
#39956=CARTESIAN_POINT ( 'NONE',  ( -1.200000000000006617, 0.000000000000000000, 0.000000000000000000 ) ) ;
#39987=EDGE_LOOP ( 'NONE', ( #20621, #7242 ) ) ;
#39995=DIRECTION ( 'NONE',  ( 0.000000000000000000, 0.000000000000000000, -1.000000000000000000 ) ) ;
#40044=DIRECTION ( 'NONE',  ( 0.000000000000000000, 0.000000000000000000, -1.000000000000000000 ) ) ;
#40053=VERTEX_POINT ( 'NONE', #60648 ) ;
#40090=ADVANCED_FACE ( 'NONE', ( #1399, #47822 ), #20539, .T. ) ;
#40124=EDGE_LOOP ( 'NONE', ( #875, #21661 ) ) ;
#40145=DIRECTION ( 'NONE',  ( 1.000000000000000000, 0.000000000000000000, 0.000000000000000000 ) ) ;
#40175=EDGE_LOOP ( 'NONE', ( #20421, #48884, #13461, #60551 ) ) ;
#40187=CARTESIAN_POINT ( 'NONE',  ( 1.500000000000000444, 6.245698675651501825E-16, 5.100000000000000533 ) ) ;
#40191=ORIENTED_EDGE ( 'NONE', *, *, #53515, .T. ) ;
#40234=CARTESIAN_POINT ( 'NONE',  ( -90.00000000000000000, 0.000000000000000000, 0.000000000000000000 ) ) ;
#40275=ORIENTED_EDGE ( 'NONE', *, *, #56286, .F. ) ;
#40387=FILL_AREA_STYLE ('',( #25031 ) ) ;
#40414=VERTEX_POINT ( 'NONE', #10448 ) ;
#40484=SHAPE_REPRESENTATION ( 'instrument roller bearing_iso_ISO 1224 - 171015 - R,24,SI,NC,24', ( #14677 ), #6659 ) ;
#40518=PLANE ( 'NONE',  #53280 ) ;
#40529=AXIS2_PLACEMENT_3D ( 'NONE', #12465, #17463, #26548 ) ;
#40600=PRODUCT_DEFINITION ( 'UNKNOWN', '', #19936, #30423 ) ;
#40791=DIRECTION ( 'NONE',  ( 0.000000000000000000, 0.000000000000000000, -1.000000000000000000 ) ) ;
#40813=ORIENTED_EDGE ( 'NONE', *, *, #22758, .F. ) ;
#40826=ADVANCED_FACE ( 'NONE', ( #52036 ), #9132, .F. ) ;
#40835=FACE_BOUND ( 'NONE', #40124, .T. ) ;
#40891=AXIS2_PLACEMENT_3D ( 'NONE', #27561, #13171, #7506 ) ;
#40950=DIRECTION ( 'NONE',  ( 1.000000000000000000, 0.000000000000000000, 0.000000000000000000 ) ) ;
#41009=CARTESIAN_POINT ( 'NONE',  ( 1.500000000000001332, 0.000000000000000000, 0.000000000000000000 ) ) ;
#41185=ORIENTED_EDGE ( 'NONE', *, *, #41485, .F. ) ;
#41230=SHAPE_DEFINITION_REPRESENTATION ( #21778, #40484 ) ;
#41276=ORIENTED_EDGE ( 'NONE', *, *, #2168, .T. ) ;
#41288=AXIS2_PLACEMENT_3D ( 'NONE', #37304, #56071, #37618 ) ;
#41295=EDGE_CURVE ( 'NONE', #40053, #23307, #699, .T. ) ;
#41315=DIRECTION ( 'NONE',  ( 1.000000000000000000, 0.000000000000000000, 0.000000000000000000 ) ) ;
#41418=ORIENTED_EDGE ( 'NONE', *, *, #49649, .T. ) ;
#41471=FACE_OUTER_BOUND ( 'NONE', #38196, .T. ) ;
#41482=ORIENTED_EDGE ( 'NONE', *, *, #32514, .F. ) ;
#41485=EDGE_CURVE ( 'NONE', #20243, #19512, #58622, .T. ) ;
#41644=EDGE_LOOP ( 'NONE', ( #37700, #41276, #1145, #58333 ) ) ;
#41739=VECTOR ( 'NONE', #4454, 1000.000000000000000 ) ;
#41797=EDGE_CURVE ( 'NONE', #8563, #219, #19773, .T. ) ;
#41884=VECTOR ( 'NONE', #8766, 1000.000000000000000 ) ;
#42008=AXIS2_PLACEMENT_3D ( 'NONE', #50548, #55547, #27368 ) ;
#42023=FACE_BOUND ( 'NONE', #43597, .T. ) ;
#42071=CIRCLE ( 'NONE', #47068, 6.728125000000022560 ) ;
#42093=DIRECTION ( 'NONE',  ( 1.000000000000000000, 0.000000000000000000, 0.000000000000000000 ) ) ;
#42153=CIRCLE ( 'NONE', #104, 0.02570000000000176310 ) ;
#42225=DIRECTION ( 'NONE',  ( 1.000000000000000000, 0.000000000000000000, 0.000000000000000000 ) ) ;
#42285=ORIENTED_EDGE ( 'NONE', *, *, #59321, .F. ) ;
#42320=EDGE_CURVE ( 'NONE', #1177, #47186, #35957, .T. ) ;
#42359=AXIS2_PLACEMENT_3D ( 'NONE', #1835, #21893, #45103 ) ;
#42483=ORIENTED_EDGE ( 'NONE', *, *, #35159, .F. ) ;
#42556=ORIENTED_EDGE ( 'NONE', *, *, #28282, .T. ) ;
#42563=CARTESIAN_POINT ( 'NONE',  ( 1.399999999999999023, 0.000000000000000000, 0.000000000000000000 ) ) ;
#42588=FACE_OUTER_BOUND ( 'NONE', #14528, .T. ) ;
#42595=CARTESIAN_POINT ( 'NONE',  ( -1.500000000000001110, 0.000000000000000000, -5.100000000000000533 ) ) ;
#42649=CARTESIAN_POINT ( 'NONE',  ( -90.00000000000000000, 6.123233995736767268E-16, 5.000000000000000888 ) ) ;
#42706=ORIENTED_EDGE ( 'NONE', *, *, #53515, .F. ) ;
#42813=ORIENTED_EDGE ( 'NONE', *, *, #43626, .T. ) ;
#42854=AXIS2_PLACEMENT_3D ( 'NONE', #21907, #60104, #13433 ) ;
#42863=CARTESIAN_POINT ( 'NONE',  ( 1.500000000000001332, 0.000000000000000000, 0.000000000000000000 ) ) ;
#42903=DIRECTION ( 'NONE',  ( 0.000000000000000000, 0.000000000000000000, -1.000000000000000000 ) ) ;
#42957=ORIENTED_EDGE ( 'NONE', *, *, #18823, .T. ) ;
#42988=DIRECTION ( 'NONE',  ( 0.000000000000000000, 0.000000000000000000, -1.000000000000000000 ) ) ;
#42990=CIRCLE ( 'NONE', #33996, 6.866799999999992465 ) ;
#43114=ORIENTED_EDGE ( 'NONE', *, *, #30537, .F. ) ;
#43150=DIRECTION ( 'NONE',  ( 0.000000000000000000, 0.000000000000000000, -1.000000000000000000 ) ) ;
#43167=CARTESIAN_POINT ( 'NONE',  ( 1.129531546211735016, 0.000000000000000000, 0.000000000000000000 ) ) ;
#43194=EDGE_CURVE ( 'NONE', #60182, #20219, #58722, .T. ) ;
#43223=DIRECTION ( 'NONE',  ( 0.000000000000000000, 0.000000000000000000, -1.000000000000000000 ) ) ;
#43343=VERTEX_POINT ( 'NONE', #12387 ) ;
#43352=DIRECTION ( 'NONE',  ( 1.000000000000000000, 0.000000000000000000, 0.000000000000000000 ) ) ;
#43404=CARTESIAN_POINT ( 'NONE',  ( 1.199999999999992628, 0.000000000000000000, 0.000000000000000000 ) ) ;
#43466=DIRECTION ( 'NONE',  ( 1.000000000000000000, 0.000000000000000000, 0.000000000000000000 ) ) ;
#43597=EDGE_LOOP ( 'NONE', ( #26630, #25674 ) ) ;
#43626=EDGE_CURVE ( 'NONE', #36274, #60182, #52920, .T. ) ;
#43694=DIRECTION ( 'NONE',  ( 1.000000000000000000, 0.000000000000000000, -0.000000000000000000 ) ) ;
#43757=CARTESIAN_POINT ( 'NONE',  ( -1.500000000000000888, 6.728125000000022560, 0.000000000000000000 ) ) ;
#43770=DIRECTION ( 'NONE',  ( 1.000000000000000000, -0.000000000000000000, -0.000000000000000000 ) ) ;
#43778=LINE ( 'NONE', #48141, #55796 ) ;
#43807=VECTOR ( 'NONE', #53927, 1000.000000000000000 ) ;
#43814=FACE_OUTER_BOUND ( 'NONE', #10375, .T. ) ;
#43832=AXIS2_PLACEMENT_3D ( 'NONE', #61235, #33690, #13654 ) ;
#43870=( GEOMETRIC_REPRESENTATION_CONTEXT ( 3 ) GLOBAL_UNCERTAINTY_ASSIGNED_CONTEXT ( ( #19209 ) ) GLOBAL_UNIT_ASSIGNED_CONTEXT ( ( #60142, #53209, #24719 ) ) REPRESENTATION_CONTEXT ( 'NONE', 'WORKASPACE' ) );
#43906=DIRECTION ( 'NONE',  ( 0.000000000000000000, 0.000000000000000000, -1.000000000000000000 ) ) ;
#43949=ORIENTED_EDGE ( 'NONE', *, *, #9500, .T. ) ;
#43989=CARTESIAN_POINT ( 'NONE',  ( -90.00000000000000000, 0.000000000000000000, 0.000000000000000000 ) ) ;
#44036=DIRECTION ( 'NONE',  ( 0.000000000000000000, 0.000000000000000000, -1.000000000000000000 ) ) ;
#44136=CARTESIAN_POINT ( 'NONE',  ( -90.00000000000000000, 0.000000000000000000, 0.000000000000000000 ) ) ;
#44172=SURFACE_STYLE_USAGE ( .BOTH. , #49752 ) ;
#44266=ORIENTED_EDGE ( 'NONE', *, *, #31259, .T. ) ;
#44268=CARTESIAN_POINT ( 'NONE',  ( 1.114300000000000068, 0.000000000000000000, 0.000000000000000000 ) ) ;
#44333=ORIENTED_EDGE ( 'NONE', *, *, #7100, .T. ) ;
#44539=EDGE_CURVE ( 'NONE', #472, #23307, #23913, .T. ) ;
#44724=EDGE_LOOP ( 'NONE', ( #7685, #16434, #14852, #45257 ) ) ;
#44731=TOROIDAL_SURFACE ( 'NONE', #36728, 5.100000000000000533, 0.1000000000000005884 ) ;
#44737=CYLINDRICAL_SURFACE ( 'NONE', #24374, 6.728125000000022560 ) ;
#44820=EDGE_LOOP ( 'NONE', ( #51518, #37412 ) ) ;
#44892=DIRECTION ( 'NONE',  ( 1.000000000000000000, 0.000000000000000000, 0.000000000000000000 ) ) ;
#44893=CARTESIAN_POINT ( 'NONE',  ( 1.129531546211735016, 6.886005254585696675E-16, 5.612499999999999822 ) ) ;
#44925=CARTESIAN_POINT ( 'NONE',  ( 1.139999999999998570, 0.000000000000000000, -6.866799999999992465 ) ) ;
#45027=DIRECTION ( 'NONE',  ( 0.000000000000000000, 0.000000000000000000, -1.000000000000000000 ) ) ;
#45064=CONICAL_SURFACE ( 'NONE', #6992, 5.453125000000000000, 0.4883339510563931007 ) ;
#45103=DIRECTION ( 'NONE',  ( 0.000000000000000000, 0.000000000000000000, -1.000000000000000000 ) ) ;
#45108=DIRECTION ( 'NONE',  ( 0.000000000000000000, 0.000000000000000000, -1.000000000000000000 ) ) ;
#45141=DIRECTION ( 'NONE',  ( 1.000000000000000000, 0.000000000000000000, 0.000000000000000000 ) ) ;
#45165=ADVANCED_FACE ( 'NONE', ( #60390 ), #29986, .T. ) ;
#45206=ORIENTED_EDGE ( 'NONE', *, *, #38363, .T. ) ;
#45257=ORIENTED_EDGE ( 'NONE', *, *, #11911, .F. ) ;
#45262=ADVANCED_FACE ( 'NONE', ( #43814 ), #52968, .T. ) ;
#45489=TOROIDAL_SURFACE ( 'NONE', #59452, 5.100000000000000533, 0.09999999999999982514 ) ;
#45605=ORIENTED_EDGE ( 'NONE', *, *, #50084, .T. ) ;
#45628=CARTESIAN_POINT ( 'NONE',  ( -90.00000000000000000, 0.000000000000000000, 0.000000000000000000 ) ) ;
#45629=EDGE_CURVE ( 'NONE', #40414, #29428, #42990, .T. ) ;
#45685=CARTESIAN_POINT ( 'NONE',  ( 1.399999999999999023, 0.000000000000000000, 0.000000000000000000 ) ) ;
#45738=EDGE_LOOP ( 'NONE', ( #33323, #41482 ) ) ;
#45770=PRESENTATION_STYLE_ASSIGNMENT (( #2815 ) ) ;
#45775=EDGE_CURVE ( 'NONE', #34877, #21245, #964, .T. ) ;
#45776=CIRCLE ( 'NONE', #18754, 5.612499999999999822 ) ;
#45810=VERTEX_POINT ( 'NONE', #22676 ) ;
#45853=CARTESIAN_POINT ( 'NONE',  ( -1.129531546211690163, 0.000000000000000000, 0.000000000000000000 ) ) ;
#45897=CARTESIAN_POINT ( 'NONE',  ( -1.200000000000006617, 8.434754829127421589E-16, 6.887500000000022382 ) ) ;
#45914=ADVANCED_FACE ( 'NONE', ( #11056, #5996 ), #20144, .T. ) ;
#45932=CARTESIAN_POINT ( 'NONE',  ( 1.199999999999992628, 0.000000000000000000, -5.612499999999999822 ) ) ;
#45952=FACE_OUTER_BOUND ( 'NONE', #50844, .T. ) ;
#45956=CIRCLE ( 'NONE', #8903, 7.500000000000022204 ) ;
#45992=FACE_OUTER_BOUND ( 'NONE', #3524, .T. ) ;
#46084=FACE_OUTER_BOUND ( 'NONE', #49644, .T. ) ;
#46091=CARTESIAN_POINT ( 'NONE',  ( -90.00000000000000000, 8.239576745513313235E-16, 6.728125000000022560 ) ) ;
#46097=DIRECTION ( 'NONE',  ( 1.000000000000000000, 0.000000000000000000, 0.000000000000000000 ) ) ;
#46163=VECTOR ( 'NONE', #20560, 1000.000000000000000 ) ;
#46275=VERTEX_POINT ( 'NONE', #27769 ) ;
#46307=ADVANCED_FACE ( 'NONE', ( #23077, #37822 ), #18381, .T. ) ;
#46364=ORIENTED_EDGE ( 'NONE', *, *, #52664, .F. ) ;
#46370=VERTEX_POINT ( 'NONE', #159 ) ;
#46381=DIRECTION ( 'NONE',  ( 1.000000000000000000, -0.000000000000000000, -0.000000000000000000 ) ) ;
#46383=ORIENTED_EDGE ( 'NONE', *, *, #39561, .F. ) ;
#46479=CIRCLE ( 'NONE', #53460, 6.728125000000023448 ) ;
#46521=DIRECTION ( 'NONE',  ( 0.000000000000000000, 0.000000000000000000, -1.000000000000000000 ) ) ;
#46541=CIRCLE ( 'NONE', #20325, 0.09999999999999939493 ) ;
#46638=ORIENTED_EDGE ( 'NONE', *, *, #42320, .F. ) ;
#46707=FACE_OUTER_BOUND ( 'NONE', #29496, .T. ) ;
#46714=VERTEX_POINT ( 'NONE', #38656 ) ;
#46719=ORIENTED_EDGE ( 'NONE', *, *, #9820, .T. ) ;
#46803=DIRECTION ( 'NONE',  ( 0.000000000000000000, 0.000000000000000000, -1.000000000000000000 ) ) ;
#46815=ORIENTED_EDGE ( 'NONE', *, *, #31136, .T. ) ;
#46835=EDGE_LOOP ( 'NONE', ( #21357, #3933 ) ) ;
#46924=CONICAL_SURFACE ( 'NONE', #53890, 5.453125000000000000, 0.4883339510563931007 ) ;
#46925=CARTESIAN_POINT ( 'NONE',  ( 1.114299999999999846, 0.000000000000000000, 0.000000000000000000 ) ) ;
#46939=CARTESIAN_POINT ( 'NONE',  ( -1.114299999999999624, 0.000000000000000000, -6.866799999999992465 ) ) ;
#47022=FACE_OUTER_BOUND ( 'NONE', #27678, .T. ) ;
#47048=LINE ( 'NONE', #42649, #25467 ) ;
#47068=AXIS2_PLACEMENT_3D ( 'NONE', #20318, #1795, #11859 ) ;
#47097=AXIS2_PLACEMENT_3D ( 'NONE', #48323, #44892, #38638 ) ;
#47169=ORIENTED_EDGE ( 'NONE', *, *, #41295, .F. ) ;
#47181=AXIS2_PLACEMENT_3D ( 'NONE', #24631, #43770, #813 ) ;
#47182=DIRECTION ( 'NONE',  ( 1.000000000000000000, -0.000000000000000000, -0.000000000000000000 ) ) ;
#47186=VERTEX_POINT ( 'NONE', #39517 ) ;
#47263=EDGE_LOOP ( 'NONE', ( #14235, #32006, #2867, #14292 ) ) ;
#47398=CARTESIAN_POINT ( 'NONE',  ( -1.200000000000006617, 0.000000000000000000, 0.000000000000000000 ) ) ;
#47439=CARTESIAN_POINT ( 'NONE',  ( 1.500000000000001332, 0.000000000000000000, 0.000000000000000000 ) ) ;
#47456=DIRECTION ( 'NONE',  ( 0.000000000000000000, 0.000000000000000000, -1.000000000000000000 ) ) ;
#47469=DIRECTION ( 'NONE',  ( 0.000000000000000000, 0.000000000000000000, -1.000000000000000000 ) ) ;
#47525=CARTESIAN_POINT ( 'NONE',  ( 1.500000000000001332, 0.000000000000000000, 5.453125000000000000 ) ) ;
#47550=VERTEX_POINT ( 'NONE', #42595 ) ;
#47577=AXIS2_PLACEMENT_3D ( 'NONE', #42863, #61916, #13733 ) ;
#47639=DIRECTION ( 'NONE',  ( 0.000000000000000000, 1.224646799147343593E-16, 1.000000000000000000 ) ) ;
#47653=ORIENTED_EDGE ( 'NONE', *, *, #32346, .T. ) ;
#47678=AXIS2_PLACEMENT_3D ( 'NONE', #50522, #7596, #27034 ) ;
#47682=DIRECTION ( 'NONE',  ( -1.000000000000000000, 0.000000000000000000, 0.000000000000000000 ) ) ;
#47701=ORIENTED_EDGE ( 'NONE', *, *, #27235, .F. ) ;
#47822=FACE_OUTER_BOUND ( 'NONE', #53826, .T. ) ;
#47948=ORIENTED_EDGE ( 'NONE', *, *, #59228, .T. ) ;
#48002=DIRECTION ( 'NONE',  ( 1.000000000000000000, 0.000000000000000000, 0.000000000000000000 ) ) ;
#48074=AXIS2_PLACEMENT_3D ( 'NONE', #53838, #34158, #291 ) ;
#48141=CARTESIAN_POINT ( 'NONE',  ( -90.00000000000000000, 0.000000000000000000, -6.887500000000022382 ) ) ;
#48195=EDGE_LOOP ( 'NONE', ( #15813, #45206, #1182, #13998 ) ) ;
#48323=CARTESIAN_POINT ( 'NONE',  ( -90.00000000000000000, 0.000000000000000000, 0.000000000000000000 ) ) ;
#48384=EDGE_CURVE ( 'NONE', #3834, #26385, #38838, .T. ) ;
#48597=CIRCLE ( 'NONE', #53585, 0.02570000000000870199 ) ;
#48620=ORIENTED_EDGE ( 'NONE', *, *, #23919, .T. ) ;
#48684=ORIENTED_EDGE ( 'NONE', *, *, #21638, .T. ) ;
#48814=VERTEX_POINT ( 'NONE', #34359 ) ;
#48884=ORIENTED_EDGE ( 'NONE', *, *, #59321, .T. ) ;
#48937=VERTEX_POINT ( 'NONE', #45932 ) ;
#49161=CARTESIAN_POINT ( 'NONE',  ( 1.199999999999992628, 0.000000000000000000, 0.000000000000000000 ) ) ;
#49166=ORIENTED_EDGE ( 'NONE', *, *, #52261, .T. ) ;
#49241=FACE_OUTER_BOUND ( 'NONE', #66, .T. ) ;
#49253=VECTOR ( 'NONE', #7524, 1000.000000000000000 ) ;
#49258=ORIENTED_EDGE ( 'NONE', *, *, #51566, .T. ) ;
#49291=CARTESIAN_POINT ( 'NONE',  ( -1.139999999999998570, 0.000000000000000000, 0.000000000000000000 ) ) ;
#49347=VECTOR ( 'NONE', #15251, 1000.000000000000000 ) ;
#49443=( NAMED_UNIT ( * ) SI_UNIT ( $, .STERADIAN. ) SOLID_ANGLE_UNIT ( ) );
#49444=FACE_OUTER_BOUND ( 'NONE', #53203, .T. ) ;
#49644=EDGE_LOOP ( 'NONE', ( #33234, #33484, #28859, #23691 ) ) ;
#49649=EDGE_CURVE ( 'NONE', #29428, #25119, #59855, .T. ) ;
#49752=SURFACE_SIDE_STYLE ('',( #11241 ) ) ;
#49765=CYLINDRICAL_SURFACE ( 'NONE', #16477, 6.728125000000023448 ) ;
#49845=CIRCLE ( 'NONE', #18877, 7.400000000000021672 ) ;
#49957=EDGE_LOOP ( 'NONE', ( #22968, #16285, #29400, #19106 ) ) ;
#50084=EDGE_CURVE ( 'NONE', #19512, #32528, #1314, .T. ) ;
#50126=VECTOR ( 'NONE', #15793, 1000.000000000000000 ) ;
#50152=DIRECTION ( 'NONE',  ( 1.000000000000000000, 0.000000000000000000, 0.000000000000000000 ) ) ;
#50216=CARTESIAN_POINT ( 'NONE',  ( -1.114299999999999846, 0.000000000000000000, -5.633200000000004870 ) ) ;
#50409=ORIENTED_EDGE ( 'NONE', *, *, #35408, .F. ) ;
#50435=ADVANCED_FACE ( 'NONE', ( #41471 ), #13261, .T. ) ;
#50443=DIRECTION ( 'NONE',  ( 0.000000000000000000, 0.000000000000000000, -1.000000000000000000 ) ) ;
#50454=APPLICATION_CONTEXT ( 'automotive_design' ) ;
#50476=EDGE_CURVE ( 'NONE', #48814, #36274, #16324, .T. ) ;
#50522=CARTESIAN_POINT ( 'NONE',  ( 1.114300000000000068, 8.409404640385035208E-16, 6.866799999999992465 ) ) ;
#50548=CARTESIAN_POINT ( 'NONE',  ( -1.500000000000001332, 0.000000000000000000, 0.000000000000000000 ) ) ;
#50641=AXIS2_PLACEMENT_3D ( 'NONE', #51094, #18228, #55179 ) ;
#50750=EDGE_CURVE ( 'NONE', #40414, #46714, #54346, .T. ) ;
#50832=ADVANCED_FACE ( 'NONE', ( #14993 ), #44737, .F. ) ;
#50844=EDGE_LOOP ( 'NONE', ( #21989, #19318, #994, #58312 ) ) ;
#50852=MECHANICAL_DESIGN_GEOMETRIC_PRESENTATION_REPRESENTATION('',(#15859),#17879);
#50970=AXIS2_PLACEMENT_3D ( 'NONE', #47398, #56166, #46803 ) ;
#50996=AXIS2_PLACEMENT_3D ( 'NONE', #8334, #56258, #22453 ) ;
#51004=DIRECTION ( 'NONE',  ( 0.000000000000000000, 1.000000000000000000, -1.224646799147353207E-16 ) ) ;
#51047=( NAMED_UNIT ( * ) PLANE_ANGLE_UNIT ( ) SI_UNIT ( $, .RADIAN. ) );
#51094=CARTESIAN_POINT ( 'NONE',  ( -1.114299999999999846, 0.000000000000000000, 0.000000000000000000 ) ) ;
#51321=ORIENTED_EDGE ( 'NONE', *, *, #37597, .T. ) ;
#51389=AXIS2_PLACEMENT_3D ( 'NONE', #45853, #47682, #23255 ) ;
#51518=ORIENTED_EDGE ( 'NONE', *, *, #44539, .F. ) ;
#51520=DIRECTION ( 'NONE',  ( 0.000000000000000000, 0.000000000000000000, -1.000000000000000000 ) ) ;
#51566=EDGE_CURVE ( 'NONE', #23307, #472, #34402, .T. ) ;
#51591=CIRCLE ( 'NONE', #7590, 5.633200000000004870 ) ;
#51617=CARTESIAN_POINT ( 'NONE',  ( 1.399999999999999023, 9.062386313690441984E-16, 7.400000000000022560 ) ) ;
#51618=ORIENTED_EDGE ( 'NONE', *, *, #24500, .F. ) ;
#51631=DIRECTION ( 'NONE',  ( 0.000000000000000000, 1.224646799147361835E-16, 1.000000000000000000 ) ) ;
#51717=AXIS2_PLACEMENT_3D ( 'NONE', #23855, #28238, #42988 ) ;
#51728=ORIENTED_EDGE ( 'NONE', *, *, #30537, .T. ) ;
#51805=ORIENTED_EDGE ( 'NONE', *, *, #48384, .F. ) ;
#51819=TOROIDAL_SURFACE ( 'NONE', #12820, 5.633200000000004870, 0.02570000000000859444 ) ;
#51861=AXIS2_PLACEMENT_3D ( 'NONE', #10153, #43694, #15171 ) ;
#51888=ADVANCED_FACE ( 'NONE', ( #1175, #1790 ), #15001, .T. ) ;
#51970=EDGE_LOOP ( 'NONE', ( #54632, #47653, #22839, #47701 ) ) ;
#52036=FACE_OUTER_BOUND ( 'NONE', #60653, .T. ) ;
#52052=DIRECTION ( 'NONE',  ( 0.000000000000000000, 0.000000000000000000, -1.000000000000000000 ) ) ;
#52127=FACE_OUTER_BOUND ( 'NONE', #38879, .T. ) ;
#52197=ORIENTED_EDGE ( 'NONE', *, *, #32790, .T. ) ;
#52234=EDGE_LOOP ( 'NONE', ( #13633, #45605, #36701, #26207 ) ) ;
#52261=EDGE_CURVE ( 'NONE', #2066, #47550, #10427, .T. ) ;
#52296=DIRECTION ( 'NONE',  ( 0.000000000000000000, 0.000000000000000000, -1.000000000000000000 ) ) ;
#52386=ORIENTED_EDGE ( 'NONE', *, *, #35159, .T. ) ;
#52621=AXIS2_PLACEMENT_3D ( 'NONE', #61301, #17486, #18417 ) ;
#52651=CARTESIAN_POINT ( 'NONE',  ( -1.500000000000001332, 0.000000000000000000, 0.000000000000000000 ) ) ;
#52664=EDGE_CURVE ( 'NONE', #19843, #15229, #25475, .T. ) ;
#52684=EDGE_CURVE ( 'NONE', #23453, #8473, #60480, .T. ) ;
#52901=DIRECTION ( 'NONE',  ( 0.000000000000000000, 0.000000000000000000, -1.000000000000000000 ) ) ;
#52920=CIRCLE ( 'NONE', #25928, 5.612499999999999822 ) ;
#52968=TOROIDAL_SURFACE ( 'NONE', #24992, 7.400000000000021672, 0.1000000000000001582 ) ;
#53104=AXIS2_PLACEMENT_3D ( 'NONE', #24171, #15410, #29181 ) ;
#53133=FACE_OUTER_BOUND ( 'NONE', #48195, .T. ) ;
#53163=ORIENTED_EDGE ( 'NONE', *, *, #32852, .T. ) ;
#53167=EDGE_CURVE ( 'NONE', #10577, #46370, #20481, .T. ) ;
#53194=ORIENTED_EDGE ( 'NONE', *, *, #56701, .T. ) ;
#53203=EDGE_LOOP ( 'NONE', ( #57779, #13535, #58820, #5533 ) ) ;
#53209=( NAMED_UNIT ( * ) PLANE_ANGLE_UNIT ( ) SI_UNIT ( $, .RADIAN. ) );
#53252=LINE ( 'NONE', #33870, #4787 ) ;
#53268=ORIENTED_EDGE ( 'NONE', *, *, #7494, .T. ) ;
#53274=DIRECTION ( 'NONE',  ( 1.000000000000000000, 0.000000000000000000, 0.000000000000000000 ) ) ;
#53280=AXIS2_PLACEMENT_3D ( 'NONE', #7258, #59582, #16691 ) ;
#53445=ORIENTED_EDGE ( 'NONE', *, *, #45629, .F. ) ;
#53460=AXIS2_PLACEMENT_3D ( 'NONE', #35095, #6850, #54152 ) ;
#53515=EDGE_CURVE ( 'NONE', #219, #8563, #46479, .T. ) ;
#53540=CIRCLE ( 'NONE', #11550, 0.09999999999999939493 ) ;
#53585=AXIS2_PLACEMENT_3D ( 'NONE', #31818, #7998, #36216 ) ;
#53777=DIRECTION ( 'NONE',  ( 1.000000000000000000, 0.000000000000000000, 0.000000000000000000 ) ) ;
#53802=CIRCLE ( 'NONE', #42854, 7.400000000000022560 ) ;
#53826=EDGE_LOOP ( 'NONE', ( #24379, #16850 ) ) ;
#53838=CARTESIAN_POINT ( 'NONE',  ( -90.00000000000000000, 0.000000000000000000, 0.000000000000000000 ) ) ;
#53890=AXIS2_PLACEMENT_3D ( 'NONE', #23885, #30113, #20120 ) ;
#53927=DIRECTION ( 'NONE',  ( 1.000000000000000000, 0.000000000000000000, 0.000000000000000000 ) ) ;
#54026=DIRECTION ( 'NONE',  ( 1.000000000000000000, 0.000000000000000000, 0.000000000000000000 ) ) ;
#54077=EDGE_LOOP ( 'NONE', ( #57011, #26449, #12816, #20963 ) ) ;
#54089=EDGE_LOOP ( 'NONE', ( #43114, #53445 ) ) ;
#54101=CARTESIAN_POINT ( 'NONE',  ( 1.500000000000001332, 0.000000000000000000, 0.000000000000000000 ) ) ;
#54119=CIRCLE ( 'NONE', #5110, 6.887500000000022382 ) ;
#54152=DIRECTION ( 'NONE',  ( 0.000000000000000000, 0.000000000000000000, -1.000000000000000000 ) ) ;
#54346=CIRCLE ( 'NONE', #17400, 0.02570000000000176310 ) ;
#54430=DIRECTION ( 'NONE',  ( 1.000000000000000000, 0.000000000000000000, 0.000000000000000000 ) ) ;
#54449=ORIENTED_EDGE ( 'NONE', *, *, #28873, .F. ) ;
#54469=AXIS2_PLACEMENT_3D ( 'NONE', #43989, #39274, #15765 ) ;
#54488=ORIENTED_EDGE ( 'NONE', *, *, #43194, .F. ) ;
#54563=ORIENTED_EDGE ( 'NONE', *, *, #59228, .F. ) ;
#54632=ORIENTED_EDGE ( 'NONE', *, *, #2768, .F. ) ;
#54698=MECHANICAL_DESIGN_GEOMETRIC_PRESENTATION_REPRESENTATION('',(#11723),#43870);
#55030=AXIS2_PLACEMENT_3D ( 'NONE', #7519, #26646, #26964 ) ;
#55037=ORIENTED_EDGE ( 'NONE', *, *, #6193, .T. ) ;
#55112=LINE ( 'NONE', #10995, #38934 ) ;
#55179=DIRECTION ( 'NONE',  ( 0.000000000000000000, 0.000000000000000000, -1.000000000000000000 ) ) ;
#55218=EDGE_LOOP ( 'NONE', ( #5842, #35111, #39497, #8718 ) ) ;
#55237=CIRCLE ( 'NONE', #10281, 5.000000000000000888 ) ;
#55299=FACE_OUTER_BOUND ( 'NONE', #33731, .T. ) ;
#55353=DIRECTION ( 'NONE',  ( 1.000000000000000000, -0.000000000000000000, -0.000000000000000000 ) ) ;
#55451=CIRCLE ( 'NONE', #20455, 5.100000000000000533 ) ;
#55477=AXIS2_PLACEMENT_3D ( 'NONE', #47439, #19251, #46521 ) ;
#55513=LINE ( 'NONE', #21709, #10887 ) ;
#55547=DIRECTION ( 'NONE',  ( 1.000000000000000000, 0.000000000000000000, 0.000000000000000000 ) ) ;
#55569=DIRECTION ( 'NONE',  ( 0.000000000000000000, -1.000000000000000000, 0.000000000000000000 ) ) ;
#55796=VECTOR ( 'NONE', #9929, 1000.000000000000000 ) ;
#55889=AXIS2_PLACEMENT_3D ( 'NONE', #1873, #45141, #11291 ) ;
#55963=ORIENTED_EDGE ( 'NONE', *, *, #38363, .F. ) ;
#56049=EDGE_LOOP ( 'NONE', ( #54488, #27416, #6299, #54563 ) ) ;
#56057=CARTESIAN_POINT ( 'NONE',  ( 1.139999999999998570, 0.000000000000000000, 0.000000000000000000 ) ) ;
#56071=DIRECTION ( 'NONE',  ( 1.000000000000000000, 0.000000000000000000, 0.000000000000000000 ) ) ;
#56093=CARTESIAN_POINT ( 'NONE',  ( -1.400000000000000799, 9.062386313690440012E-16, 7.400000000000021672 ) ) ;
#56128=CARTESIAN_POINT ( 'NONE',  ( -1.114299999999999624, 0.000000000000000000, 0.000000000000000000 ) ) ;
#56148=DIRECTION ( 'NONE',  ( -0.000000000000000000, -1.000000000000000000, -0.000000000000000000 ) ) ;
#56166=DIRECTION ( 'NONE',  ( 1.000000000000000000, 0.000000000000000000, 0.000000000000000000 ) ) ;
#56220=PRODUCT_CONTEXT ( 'NONE', #33157, 'mechanical' ) ;
#56252=FACE_OUTER_BOUND ( 'NONE', #49957, .T. ) ;
#56258=DIRECTION ( 'NONE',  ( 1.000000000000000000, 0.000000000000000000, 0.000000000000000000 ) ) ;
#56273=ORIENTED_EDGE ( 'NONE', *, *, #30896, .T. ) ;
#56286=EDGE_CURVE ( 'NONE', #22147, #59631, #31615, .T. ) ;
#56329=AXIS2_PLACEMENT_3D ( 'NONE', #17962, #56148, #32364 ) ;
#56373=DIRECTION ( 'NONE',  ( 0.000000000000000000, 0.000000000000000000, -1.000000000000000000 ) ) ;
#56379=DIRECTION ( 'NONE',  ( 0.000000000000000000, 0.000000000000000000, -1.000000000000000000 ) ) ;
#56631=ADVANCED_FACE ( 'NONE', ( #53133 ), #1583, .T. ) ;
#56701=EDGE_CURVE ( 'NONE', #25197, #60182, #48597, .T. ) ;
#56708=EDGE_LOOP ( 'NONE', ( #51728, #8783, #39320, #30070 ) ) ;
#56756=CIRCLE ( 'NONE', #35783, 5.612499999999999822 ) ;
#56833=CYLINDRICAL_SURFACE ( 'NONE', #13770, 5.612499999999999822 ) ;
#56973=EDGE_LOOP ( 'NONE', ( #19582, #15423, #41418, #17916 ) ) ;
#57011=ORIENTED_EDGE ( 'NONE', *, *, #18823, .F. ) ;
#57042=CIRCLE ( 'NONE', #6000, 6.728125000000022560 ) ;
#57136=CARTESIAN_POINT ( 'NONE',  ( -1.114299999999999846, 6.898680348956876061E-16, 5.633200000000004870 ) ) ;
#57253=CARTESIAN_POINT ( 'NONE',  ( 1.129531546211735016, 0.000000000000000000, -5.612499999999999822 ) ) ;
#57322=EDGE_CURVE ( 'NONE', #26385, #47550, #58505, .T. ) ;
#57647=CIRCLE ( 'NONE', #3638, 6.887500000000022382 ) ;
#57779=ORIENTED_EDGE ( 'NONE', *, *, #8512, .F. ) ;
#57842=CARTESIAN_POINT ( 'NONE',  ( -1.500000000000001332, 0.000000000000000000, -5.453125000000000000 ) ) ;
#57921=DIRECTION ( 'NONE',  ( -0.000000000000000000, 0.000000000000000000, 1.000000000000000000 ) ) ;
#57975=AXIS2_PLACEMENT_3D ( 'NONE', #34987, #12404, #15868 ) ;
#58122=CARTESIAN_POINT ( 'NONE',  ( -1.139999999999998570, 0.000000000000000000, 0.000000000000000000 ) ) ;
#58125=CARTESIAN_POINT ( 'NONE',  ( -1.399999999999998579, 0.000000000000000000, 0.000000000000000000 ) ) ;
#58164=DIRECTION ( 'NONE',  ( 1.000000000000000000, 0.000000000000000000, 0.000000000000000000 ) ) ;
#58210=PRESENTATION_STYLE_ASSIGNMENT (( #44172 ) ) ;
#58243=EDGE_CURVE ( 'NONE', #39657, #58899, #13510, .T. ) ;
#58312=ORIENTED_EDGE ( 'NONE', *, *, #32543, .F. ) ;
#58333=ORIENTED_EDGE ( 'NONE', *, *, #32852, .F. ) ;
#58374=DIRECTION ( 'NONE',  ( 0.000000000000000000, -1.000000000000000000, 0.000000000000000000 ) ) ;
#58410=DIRECTION ( 'NONE',  ( 1.000000000000000000, 0.000000000000000000, 0.000000000000000000 ) ) ;
#58501=AXIS2_PLACEMENT_3D ( 'NONE', #1563, #5630, #26012 ) ;
#58505=CIRCLE ( 'NONE', #1444, 5.100000000000000533 ) ;
#58622=LINE ( 'NONE', #34859, #43807 ) ;
#58655=CARTESIAN_POINT ( 'NONE',  ( -1.500000000000001332, 8.239576745513313235E-16, 6.728125000000022560 ) ) ;
#58722=LINE ( 'NONE', #6396, #26870 ) ;
#58784=AXIS2_PLACEMENT_3D ( 'NONE', #4262, #42225, #23399 ) ;
#58820=ORIENTED_EDGE ( 'NONE', *, *, #36296, .T. ) ;
#58843=COLOUR_RGB ( '', 0.40784314, 0.44705882, 0.49803922) ;
#58844=DIRECTION ( 'NONE',  ( 1.000000000000000000, 0.000000000000000000, 0.000000000000000000 ) ) ;
#58899=VERTEX_POINT ( 'NONE', #40187 ) ;
#58910=AXIS2_PLACEMENT_3D ( 'NONE', #37478, #36865, #31519 ) ;
#59149=CARTESIAN_POINT ( 'NONE',  ( -90.00000000000000000, 0.000000000000000000, 0.000000000000000000 ) ) ;
#59228=EDGE_CURVE ( 'NONE', #20219, #48937, #518, .T. ) ;
#59321=EDGE_CURVE ( 'NONE', #22775, #46370, #53540, .T. ) ;
#59351=CIRCLE ( 'NONE', #10373, 7.500000000000022204 ) ;
#59412=AXIS2_PLACEMENT_3D ( 'NONE', #25611, #20015, #25302 ) ;
#59429=ADVANCED_BREP_SHAPE_REPRESENTATION ( '', ( #10859, #14677 ), #6659 ) ;
#59440=FACE_OUTER_BOUND ( 'NONE', #40175, .T. ) ;
#59452=AXIS2_PLACEMENT_3D ( 'NONE', #6543, #35416, #38891 ) ;
#59518=CARTESIAN_POINT ( 'NONE',  ( -90.00000000000000000, 8.434754829127421589E-16, 6.887500000000022382 ) ) ;
#59582=DIRECTION ( 'NONE',  ( -1.000000000000000000, 0.000000000000000000, 0.000000000000000000 ) ) ;
#59631=VERTEX_POINT ( 'NONE', #17129 ) ;
#59742=ADVANCED_FACE ( 'NONE', ( #18673 ), #15615, .T. ) ;
#59743=DIRECTION ( 'NONE',  ( -1.000000000000000000, -0.000000000000000000, -0.000000000000000000 ) ) ;
#59840=CARTESIAN_POINT ( 'NONE',  ( 1.500000000000001332, 0.000000000000000000, -7.400000000000022560 ) ) ;
#59855=CIRCLE ( 'NONE', #17845, 0.02570000000000176310 ) ;
#59971=CARTESIAN_POINT ( 'NONE',  ( 1.500000000000001332, 0.000000000000000000, -6.728125000000023448 ) ) ;
#60038=CARTESIAN_POINT ( 'NONE',  ( -90.00000000000000000, 0.000000000000000000, -6.728125000000022560 ) ) ;
#60104=DIRECTION ( 'NONE',  ( 1.000000000000000000, 0.000000000000000000, 0.000000000000000000 ) ) ;
#60142=( LENGTH_UNIT ( ) NAMED_UNIT ( * ) SI_UNIT ( .MILLI., .METRE. ) );
#60182=VERTEX_POINT ( 'NONE', #44893 ) ;
#60390=FACE_OUTER_BOUND ( 'NONE', #13262, .T. ) ;
#60480=CIRCLE ( 'NONE', #4435, 5.000000000000000888 ) ;
#60514=DIRECTION ( 'NONE',  ( 1.000000000000000000, 0.000000000000000000, 0.000000000000000000 ) ) ;
#60551=ORIENTED_EDGE ( 'NONE', *, *, #21638, .F. ) ;
#60637=ADVANCED_FACE ( 'NONE', ( #56252 ), #25613, .T. ) ;
#60648=CARTESIAN_POINT ( 'NONE',  ( 1.129531546211701931, 8.434754829127421589E-16, 6.887500000000022382 ) ) ;
#60653=EDGE_LOOP ( 'NONE', ( #8671, #40813, #36632, #38103 ) ) ;
#60767=DIRECTION ( 'NONE',  ( 1.000000000000000000, -0.000000000000000000, -0.000000000000000000 ) ) ;
#60824=DIRECTION ( 'NONE',  ( 0.000000000000000000, 0.000000000000000000, -1.000000000000000000 ) ) ;
#60897=VERTEX_POINT ( 'NONE', #17675 ) ;
#61018=VERTEX_POINT ( 'NONE', #45897 ) ;
#61024=TOROIDAL_SURFACE ( 'NONE', #35077, 6.866799999999992465, 0.02570000000000859444 ) ;
#61084=CARTESIAN_POINT ( 'NONE',  ( 1.500000000000001332, 0.000000000000000000, 5.453125000000000000 ) ) ;
#61235=CARTESIAN_POINT ( 'NONE',  ( -1.500000000000001332, 0.000000000000000000, 0.000000000000000000 ) ) ;
#61301=CARTESIAN_POINT ( 'NONE',  ( 1.114300000000000068, 0.000000000000000000, -6.866799999999992465 ) ) ;
#61306=ADVANCED_FACE ( 'NONE', ( #7883 ), #7620, .T. ) ;
#61329=ORIENTED_EDGE ( 'NONE', *, *, #27858, .T. ) ;
#61387=DIRECTION ( 'NONE',  ( 0.000000000000000000, 0.000000000000000000, 1.000000000000000000 ) ) ;
#61639=ADVANCED_FACE ( 'NONE', ( #19387 ), #44731, .T. ) ;
#61670=ORIENTED_EDGE ( 'NONE', *, *, #12262, .T. ) ;
#61715=VECTOR ( 'NONE', #3320, 1000.000000000000000 ) ;
#61755=VERTEX_POINT ( 'NONE', #59971 ) ;
#61867=ORIENTED_EDGE ( 'NONE', *, *, #6193, .F. ) ;
#61895=CARTESIAN_POINT ( 'NONE',  ( -1.399999999999998579, 0.000000000000000000, 0.000000000000000000 ) ) ;
#61916=DIRECTION ( 'NONE',  ( 1.000000000000000000, 0.000000000000000000, 0.000000000000000000 ) ) ;
ENDSEC;
END-ISO-10303-21;
